ISO-10303-21;
HEADER;
FILE_DESCRIPTION (('STEP AP214'),
    '1' );
FILE_NAME ('Reach Screw.step',
    '2026-10-30T09:41:00',
    ( '' ),
    ( '' ),
    'SwSTEP 2.0',
    'SolidWorks 2020',
    '' );
FILE_SCHEMA (( 'AUTOMOTIVE_DESIGN' ));
ENDSEC;

DATA;
#8=DIRECTION ( 'NONE',  ( 1.000000000000000000, 0.000000000000000000, -0.000000000000000000 ) ) ;
#14=CIRCLE ( 'NONE', #29859, 2.000000000000000444 ) ;
#16=CARTESIAN_POINT ( 'NONE',  ( 89.67401078471493747, -27.84333996136784961, -14.15691383771150136 ) ) ;
#17=VERTEX_POINT ( 'NONE', #2774 ) ;
#23=ORIENTED_EDGE ( 'NONE', *, *, #16097, .T. ) ;
#29=EDGE_CURVE ( 'NONE', #24368, #33578, #9787, .T. ) ;
#51=ADVANCED_FACE ( 'NONE', ( #30593 ), #44511, .T. ) ;
#64=AXIS2_PLACEMENT_3D ( 'NONE', #36243, #40129, #40585 ) ;
#72=ORIENTED_EDGE ( 'NONE', *, *, #6315, .T. ) ;
#138=LINE ( 'NONE', #803, #41193 ) ;
#139=DIRECTION ( 'NONE',  ( 0.000000000000000000, 0.9242245927363041957, 0.3818493186865896116 ) ) ;
#161=DIRECTION ( 'NONE',  ( 0.000000000000000000, -0.3818493186865927203, 0.9242245927363029745 ) ) ;
#206=CARTESIAN_POINT ( 'NONE',  ( 90.99708770779186295, -25.99489077589524300, -13.39321520033831447 ) ) ;
#209=ORIENTED_EDGE ( 'NONE', *, *, #44836, .F. ) ;
#230=AXIS2_PLACEMENT_3D ( 'NONE', #1932, #32931, #26795 ) ;
#232=CONICAL_SURFACE ( 'NONE', #26442, 1.610000000000000986, 0.9599310885968765916 ) ;
#239=ADVANCED_FACE ( 'NONE', ( #9623 ), #30148, .T. ) ;
#245=AXIS2_PLACEMENT_3D ( 'NONE', #38694, #8154, #22058 ) ;
#246=ORIENTED_EDGE ( 'NONE', *, *, #30782, .T. ) ;
#271=CARTESIAN_POINT ( 'NONE',  ( 91.77400275106518279, -25.99489077589524300, -13.39321520033831625 ) ) ;
#301=EDGE_CURVE ( 'NONE', #24082, #31284, #22134, .T. ) ;
#315=CARTESIAN_POINT ( 'NONE',  ( 121.9470836909669913, -25.99489077589524300, -13.39321520033831447 ) ) ;
#317=CARTESIAN_POINT ( 'NONE',  ( 90.04708369096697140, -25.99489077589524300, -13.39321520033831447 ) ) ;
#329=ORIENTED_EDGE ( 'NONE', *, *, #34728, .F. ) ;
#357=DIRECTION ( 'NONE',  ( 1.000000000000000000, 0.000000000000000000, -0.000000000000000000 ) ) ;
#358=CARTESIAN_POINT ( 'NONE',  ( 94.20708369096698220, -26.09538666226425363, -14.49867541642786861 ) ) ;
#366=CARTESIAN_POINT ( 'NONE',  ( 95.28169473643895060, -25.99489077589524300, -13.39321520033831447 ) ) ;
#373=ORIENTED_EDGE ( 'NONE', *, *, #35321, .F. ) ;
#379=CARTESIAN_POINT ( 'NONE',  ( 96.46827370896536991, -26.13949388144357755, -14.39191870720298994 ) ) ;
#422=DIRECTION ( 'NONE',  ( 1.000000000000000000, 0.000000000000000000, -0.000000000000000000 ) ) ;
#427=FACE_OUTER_BOUND ( 'NONE', #35725, .T. ) ;
#437=CARTESIAN_POINT ( 'NONE',  ( 85.15861813568058380, -26.75858941326842810, -11.54476601486570964 ) ) ;
#439=DIRECTION ( 'NONE',  ( 1.000000000000000000, 0.000000000000000000, -0.000000000000000000 ) ) ;
#468=DIRECTION ( 'NONE',  ( 0.000000000000000000, -0.3818493186865927203, 0.9242245927363029745 ) ) ;
#480=EDGE_LOOP ( 'NONE', ( #674, #23, #42394, #32349, #19349 ) ) ;
#481=VECTOR ( 'NONE', #10247, 1000.000000000000000 ) ;
#489=ORIENTED_EDGE ( 'NONE', *, *, #38798, .T. ) ;
#501=ORIENTED_EDGE ( 'NONE', *, *, #21109, .T. ) ;
#508=CYLINDRICAL_SURFACE ( 'NONE', #17648, 1.999999999999998890 ) ;
#543=DIRECTION ( 'NONE',  ( 1.000000000000000000, 0.000000000000000000, -0.000000000000000000 ) ) ;
#592=DIRECTION ( 'NONE',  ( -1.224775218828351862E-16, 0.3818493186865896671, -0.9242245927363043068 ) ) ;
#604=DIRECTION ( 'NONE',  ( -1.000000000000000000, 0.000000000000000000, 0.000000000000000000 ) ) ;
#618=ORIENTED_EDGE ( 'NONE', *, *, #13638, .T. ) ;
#619=DIRECTION ( 'NONE',  ( 1.000000000000000000, 0.000000000000000000, -0.000000000000000000 ) ) ;
#672=DIRECTION ( 'NONE',  ( -0.5735764363510450492, -0.3127926500124816878, 0.7570804645221038687 ) ) ;
#674=ORIENTED_EDGE ( 'NONE', *, *, #40341, .T. ) ;
#683=ORIENTED_EDGE ( 'NONE', *, *, #19629, .T. ) ;
#691=DIRECTION ( 'NONE',  ( 1.000000000000000000, 0.000000000000000000, -0.000000000000000000 ) ) ;
#717=CARTESIAN_POINT ( 'NONE',  ( 89.12784890491134604, -25.99489077589524300, -13.39321520033831625 ) ) ;
#720=AXIS2_PLACEMENT_3D ( 'NONE', #5243, #1374, #19159 ) ;
#732=DIRECTION ( 'NONE',  ( 1.000000000000000000, 0.000000000000000000, -0.000000000000000000 ) ) ;
#735=VERTEX_POINT ( 'NONE', #8443 ) ;
#753=CIRCLE ( 'NONE', #18249, 1.610000000000000986 ) ;
#782=EDGE_CURVE ( 'NONE', #20212, #40139, #9055, .T. ) ;
#785=CIRCLE ( 'NONE', #6628, 1.009117809157100254 ) ;
#790=EDGE_CURVE ( 'NONE', #42505, #31077, #32347, .T. ) ;
#791=CONICAL_SURFACE ( 'NONE', #29218, 1.610000000000000986, 0.9599310885968765916 ) ;
#795=CIRCLE ( 'NONE', #27739, 2.000000000000000444 ) ;
#803=CARTESIAN_POINT ( 'NONE',  ( 121.9470836909669913, -27.84333996136784961, -14.15691383771150136 ) ) ;
#837=ORIENTED_EDGE ( 'NONE', *, *, #6922, .T. ) ;
#849=ORIENTED_EDGE ( 'NONE', *, *, #34615, .T. ) ;
#850=SHAPE_REPRESENTATION ( 'Reach Screw', ( #12375 ), #43820 ) ;
#858=DIRECTION ( 'NONE',  ( 0.000000000000000000, -0.9242245927363029745, -0.3818493186865927203 ) ) ;
#890=AXIS2_PLACEMENT_3D ( 'NONE', #38470, #13662, #21159 ) ;
#895=FILL_AREA_STYLE ('',( #36665 ) ) ;
#897=LINE ( 'NONE', #21877, #4551 ) ;
#902=EDGE_CURVE ( 'NONE', #31222, #12871, #2499, .T. ) ;
#917=PRODUCT_DEFINITION_FORMATION_WITH_SPECIFIED_SOURCE ( 'ANY', '', #14299, .NOT_KNOWN. ) ;
#918=CARTESIAN_POINT ( 'NONE',  ( 91.65862616933031859, -25.99489077589524300, -13.39321520033831447 ) ) ;
#952=AXIS2_PLACEMENT_3D ( 'NONE', #12557, #23033, #37617 ) ;
#965=DIRECTION ( 'NONE',  ( 1.000000000000000000, 0.000000000000000000, 0.000000000000000000 ) ) ;
#969=ORIENTED_EDGE ( 'NONE', *, *, #34509, .F. ) ;
#977=VECTOR ( 'NONE', #13213, 1000.000000000000114 ) ;
#978=DIRECTION ( 'NONE',  ( -0.5735764363510450492, -0.3127926500124816878, 0.7570804645221038687 ) ) ;
#986=ORIENTED_EDGE ( 'NONE', *, *, #21820, .F. ) ;
#1000=DIRECTION ( 'NONE',  ( 1.000000000000000000, 0.000000000000000000, -0.000000000000000000 ) ) ;
#1019=ORIENTED_EDGE ( 'NONE', *, *, #38423, .F. ) ;
#1022=CARTESIAN_POINT ( 'NONE',  ( 95.28169473643895060, -27.46631665213706341, -9.831789489566176599 ) ) ;
#1024=DIRECTION ( 'NONE',  ( -1.000000000000000000, 0.000000000000000000, 0.000000000000000000 ) ) ;
#1042=VERTEX_POINT ( 'NONE', #3175 ) ;
#1066=ORIENTED_EDGE ( 'NONE', *, *, #25382, .T. ) ;
#1105=FACE_OUTER_BOUND ( 'NONE', #32890, .T. ) ;
#1110=PLANE ( 'NONE',  #3169 ) ;
#1121=EDGE_CURVE ( 'NONE', #44907, #4162, #20514, .T. ) ;
#1123=CARTESIAN_POINT ( 'NONE',  ( 84.10862215250544693, -25.38011337280982715, -14.88121679464376257 ) ) ;
#1161=ORIENTED_EDGE ( 'NONE', *, *, #24252, .F. ) ;
#1164=CARTESIAN_POINT ( 'NONE',  ( 85.15861813568058380, -25.99489077589524300, -13.39321520033831625 ) ) ;
#1166=( GEOMETRIC_REPRESENTATION_CONTEXT ( 3 ) GLOBAL_UNCERTAINTY_ASSIGNED_CONTEXT ( ( #25138 ) ) GLOBAL_UNIT_ASSIGNED_CONTEXT ( ( #7965, #1788, #11846 ) ) REPRESENTATION_CONTEXT ( 'NONE', 'WORKASPACE' ) );
#1178=CIRCLE ( 'NONE', #8439, 2.000000000000000444 ) ;
#1179=ADVANCED_FACE ( 'NONE', ( #32760 ), #18434, .T. ) ;
#1184=ORIENTED_EDGE ( 'NONE', *, *, #30337, .F. ) ;
#1188=DIRECTION ( 'NONE',  ( 1.000000000000000000, 0.000000000000000000, -0.000000000000000000 ) ) ;
#1291=FACE_OUTER_BOUND ( 'NONE', #9136, .T. ) ;
#1344=DIRECTION ( 'NONE',  ( 0.000000000000000000, -0.3818493186865927203, 0.9242245927363029745 ) ) ;
#1346=EDGE_CURVE ( 'NONE', #29689, #5805, #26565, .T. ) ;
#1356=EDGE_CURVE ( 'NONE', #23574, #14619, #40404, .T. ) ;
#1363=EDGE_CURVE ( 'NONE', #2333, #17, #20035, .T. ) ;
#1374=DIRECTION ( 'NONE',  ( -1.000000000000000000, 0.000000000000000000, 0.000000000000000000 ) ) ;
#1382=ORIENTED_EDGE ( 'NONE', *, *, #8038, .F. ) ;
#1385=FACE_OUTER_BOUND ( 'NONE', #41858, .T. ) ;
#1393=ORIENTED_EDGE ( 'NONE', *, *, #39499, .F. ) ;
#1394=DIRECTION ( 'NONE',  ( 1.000000000000000000, 0.000000000000000000, -0.000000000000000000 ) ) ;
#1406=AXIS2_PLACEMENT_3D ( 'NONE', #27701, #24497, #41617 ) ;
#1433=AXIS2_PLACEMENT_3D ( 'NONE', #39088, #10833, #7857 ) ;
#1467=CARTESIAN_POINT ( 'NONE',  ( 86.36631847702263087, -24.14644159042263993, -12.62951656296512937 ) ) ;
#1486=ORIENTED_EDGE ( 'NONE', *, *, #19177, .T. ) ;
#1509=CARTESIAN_POINT ( 'NONE',  ( 88.73939138327467901, -25.99489077589524300, -13.39321520033831625 ) ) ;
#1511=DIRECTION ( 'NONE',  ( 1.000000000000000000, 0.000000000000000000, -0.000000000000000000 ) ) ;
#1522=VERTEX_POINT ( 'NONE', #26391 ) ;
#1535=CONICAL_SURFACE ( 'NONE', #19024, 1.610000000000000986, 0.9599310885968765916 ) ;
#1548=DIRECTION ( 'NONE',  ( 0.000000000000000000, -0.3818493186865936084, 0.9242245927363024194 ) ) ;
#1580=CARTESIAN_POINT ( 'NONE',  ( 90.04708369096697140, -26.47086644115443832, -13.58986759946190936 ) ) ;
#1593=EDGE_CURVE ( 'NONE', #32925, #4162, #18559, .T. ) ;
#1647=EDGE_LOOP ( 'NONE', ( #35667, #1161, #32807, #7658, #11034 ) ) ;
#1649=CIRCLE ( 'NONE', #24971, 1.009117809157100254 ) ;
#1677=ORIENTED_EDGE ( 'NONE', *, *, #32967, .T. ) ;
#1695=AXIS2_PLACEMENT_3D ( 'NONE', #3814, #41697, #20721 ) ;
#1701=ORIENTED_EDGE ( 'NONE', *, *, #37070, .T. ) ;
#1733=DIRECTION ( 'NONE',  ( 0.000000000000000000, -0.3818493186865936084, 0.9242245927363024194 ) ) ;
#1737=EDGE_CURVE ( 'NONE', #35629, #35146, #2039, .T. ) ;
#1745=CARTESIAN_POINT ( 'NONE',  ( 85.04324155394569118, -25.99489077589524300, -13.39321520033831447 ) ) ;
#1748=PLANE ( 'NONE',  #11154 ) ;
#1771=DIRECTION ( 'NONE',  ( 1.000000000000000000, 0.000000000000000000, -0.000000000000000000 ) ) ;
#1781=AXIS2_PLACEMENT_3D ( 'NONE', #24597, #16874, #38481 ) ;
#1788=( NAMED_UNIT ( * ) PLANE_ANGLE_UNIT ( ) SI_UNIT ( $, .RADIAN. ) );
#1803=CARTESIAN_POINT ( 'NONE',  ( 93.93057702947278642, -25.99489077589524300, -13.39321520033831447 ) ) ;
#1804=CARTESIAN_POINT ( 'NONE',  ( 89.01247232317646763, -25.99489077589524300, -13.39321520033831447 ) ) ;
#1815=DIRECTION ( 'NONE',  ( -0.5735764363510446051, 0.3127926500124816878, -0.7570804645221042017 ) ) ;
#1827=CYLINDRICAL_SURFACE ( 'NONE', #3016, 1.999999999999998890 ) ;
#1842=ORIENTED_EDGE ( 'NONE', *, *, #22274, .T. ) ;
#1848=DIRECTION ( 'NONE',  ( 0.000000000000000000, -0.9242245927363027524, -0.3818493186865928868 ) ) ;
#1850=ADVANCED_FACE ( 'NONE', ( #27747 ), #30965, .T. ) ;
#1863=ADVANCED_FACE ( 'NONE', ( #17044 ), #6316, .T. ) ;
#1874=DIRECTION ( 'NONE',  ( 0.000000000000000000, -0.3818493186865936084, 0.9242245927363024194 ) ) ;
#1880=DIRECTION ( 'NONE',  ( 1.000000000000000000, 0.000000000000000000, -0.000000000000000000 ) ) ;
#1890=AXIS2_PLACEMENT_3D ( 'NONE', #13306, #3694, #31285 ) ;
#1917=AXIS2_PLACEMENT_3D ( 'NONE', #9833, #40844, #41736 ) ;
#1923=CARTESIAN_POINT ( 'NONE',  ( 121.9470836909669913, -22.29799240495002977, -11.86581792559194426 ) ) ;
#1932=CARTESIAN_POINT ( 'NONE',  ( 90.06246830635160450, -25.99489077589524300, -13.39321520033831625 ) ) ;
#1954=LINE ( 'NONE', #12463, #15351 ) ;
#1963=SHAPE_DEFINITION_REPRESENTATION ( #18316, #850 ) ;
#1991=ORIENTED_EDGE ( 'NONE', *, *, #13608, .T. ) ;
#2001=DIRECTION ( 'NONE',  ( 1.000000000000000000, 0.000000000000000000, -0.000000000000000000 ) ) ;
#2010=AXIS2_PLACEMENT_3D ( 'NONE', #28863, #15173, #18817 ) ;
#2011=CARTESIAN_POINT ( 'NONE',  ( 87.80477198183443477, -25.99489077589524300, -13.39321520033831625 ) ) ;
#2024=ORIENTED_EDGE ( 'NONE', *, *, #10295, .T. ) ;
#2031=DIRECTION ( 'NONE',  ( 1.000000000000000000, 0.000000000000000000, -0.000000000000000000 ) ) ;
#2039=B_SPLINE_CURVE_WITH_KNOTS ( 'NONE', 3,
 ( #14055, #34342, #44860, #13399 ),
 .UNSPECIFIED., .F., .F.,
 ( 4, 4 ),
 ( 0.000000000000000000, 1.000000000000000000 ),
 .UNSPECIFIED. ) ;
#2069=CARTESIAN_POINT ( 'NONE',  ( 85.04324155394569118, -26.75858941326842810, -11.54476601486570964 ) ) ;
#2087=PLANE ( 'NONE',  #6903 ) ;
#2096=ORIENTED_EDGE ( 'NONE', *, *, #43220, .F. ) ;
#2138=CIRCLE ( 'NONE', #36344, 6.479565957685750277 ) ;
#2150=LINE ( 'NONE', #33157, #11976 ) ;
#2193=CARTESIAN_POINT ( 'NONE',  ( 87.41631446019775353, -26.60966817898065884, -11.90521360603286816 ) ) ;
#2194=VERTEX_POINT ( 'NONE', #12208 ) ;
#2205=CONICAL_SURFACE ( 'NONE', #44488, 1.610000000000000986, 0.9599310885968765916 ) ;
#2246=LINE ( 'NONE', #37120, #977 ) ;
#2257=DIRECTION ( 'NONE',  ( 1.000000000000000000, 0.000000000000000000, -0.000000000000000000 ) ) ;
#2285=EDGE_CURVE ( 'NONE', #42482, #30793, #33836, .T. ) ;
#2304=ORIENTED_EDGE ( 'NONE', *, *, #38190, .T. ) ;
#2311=AXIS2_PLACEMENT_3D ( 'NONE', #37760, #732, #28339 ) ;
#2333=VERTEX_POINT ( 'NONE', #13563 ) ;
#2336=DIRECTION ( 'NONE',  ( -0.000000000000000000, -0.3818493186865896671, 0.9242245927363040847 ) ) ;
#2406=ORIENTED_EDGE ( 'NONE', *, *, #30337, .T. ) ;
#2423=ORIENTED_EDGE ( 'NONE', *, *, #5411, .T. ) ;
#2427=CARTESIAN_POINT ( 'NONE',  ( 85.82015659721905365, -25.99489077589524300, -13.39321520033831625 ) ) ;
#2441=VERTEX_POINT ( 'NONE', #30434 ) ;
#2446=ADVANCED_FACE ( 'NONE', ( #23836 ), #34069, .T. ) ;
#2482=ORIENTED_EDGE ( 'NONE', *, *, #5224, .F. ) ;
#2499=CIRCLE ( 'NONE', #1781, 2.000000000000000444 ) ;
#2504=DIRECTION ( 'NONE',  ( 1.000000000000000000, 0.000000000000000000, -0.000000000000000000 ) ) ;
#2518=CARTESIAN_POINT ( 'NONE',  ( 93.44708369096697709, -23.96159667187537679, -12.55314669922780979 ) ) ;
#2541=CARTESIAN_POINT ( 'NONE',  ( 85.43169907558235820, -25.99489077589524300, -13.39321520033831625 ) ) ;
#2542=EDGE_CURVE ( 'NONE', #17, #4318, #3287, .T. ) ;
#2565=DIRECTION ( 'NONE',  ( 0.5735764363510499342, 0.3127926500124801890, -0.7570804645221008711 ) ) ;
#2572=VERTEX_POINT ( 'NONE', #27921 ) ;
#2587=VERTEX_POINT ( 'NONE', #32603 ) ;
#2588=DIRECTION ( 'NONE',  ( 1.000000000000000000, 0.000000000000000000, -0.000000000000000000 ) ) ;
#2616=CYLINDRICAL_SURFACE ( 'NONE', #6503, 1.999999999999998890 ) ;
#2651=AXIS2_PLACEMENT_3D ( 'NONE', #8393, #4736, #29364 ) ;
#2661=CARTESIAN_POINT ( 'NONE',  ( 94.99177781699742695, -25.99489077589524300, -13.39321520033831447 ) ) ;
#2689=AXIS2_PLACEMENT_3D ( 'NONE', #19513, #5144, #12230 ) ;
#2702=EDGE_LOOP ( 'NONE', ( #16935, #35690, #26572, #28944, #26319, #39425 ) ) ;
#2711=CIRCLE ( 'NONE', #38373, 2.000000000000000444 ) ;
#2712=CARTESIAN_POINT ( 'NONE',  ( 90.45092582798827152, -25.23119213852205789, -15.24166438581092109 ) ) ;
#2715=DIRECTION ( 'NONE',  ( 0.000000000000000000, -0.9242245927363029745, -0.3818493186865927758 ) ) ;
#2719=FACE_OUTER_BOUND ( 'NONE', #35178, .T. ) ;
#2728=EDGE_LOOP ( 'NONE', ( #24589, #42370, #39697, #41041, #8031 ) ) ;
#2731=ADVANCED_FACE ( 'NONE', ( #28250 ), #4742, .T. ) ;
#2742=EDGE_CURVE ( 'NONE', #41727, #37027, #24256, .T. ) ;
#2752=DIRECTION ( 'NONE',  ( 1.000000000000000000, 0.000000000000000000, -0.000000000000000000 ) ) ;
#2756=EDGE_CURVE ( 'NONE', #29406, #5805, #23817, .T. ) ;
#2765=ADVANCED_FACE ( 'NONE', ( #3491 ), #31297, .T. ) ;
#2774=CARTESIAN_POINT ( 'NONE',  ( 86.09323753712084226, -26.60966817898065884, -11.90521360603286816 ) ) ;
#2784=EDGE_LOOP ( 'NONE', ( #37832, #25173, #5289, #36988 ) ) ;
#2800=CARTESIAN_POINT ( 'NONE',  ( 90.33554924625337890, -27.84333996136784961, -14.15691383771150136 ) ) ;
#2804=CARTESIAN_POINT ( 'NONE',  ( 90.99708770779186295, -24.14644159042263993, -12.62951656296512937 ) ) ;
#2823=EDGE_CURVE ( 'NONE', #8410, #10961, #42247, .T. ) ;
#2834=ORIENTED_EDGE ( 'NONE', *, *, #21144, .F. ) ;
#2838=CARTESIAN_POINT ( 'NONE',  ( 91.65862616933031859, -25.99489077589524300, -13.39321520033831447 ) ) ;
#2842=AXIS2_PLACEMENT_3D ( 'NONE', #25697, #1511, #1733 ) ;
#2844=VERTEX_POINT ( 'NONE', #20387 ) ;
#2863=CARTESIAN_POINT ( 'NONE',  ( 93.24708369096698846, -27.84333996136784961, -14.15691383771150136 ) ) ;
#2864=ADVANCED_FACE ( 'NONE', ( #7351 ), #27897, .T. ) ;
#2877=CIRCLE ( 'NONE', #26965, 1.610000000000000986 ) ;
#2908=DIRECTION ( 'NONE',  ( 0.000000000000000000, -0.3818493186865927203, 0.9242245927363029745 ) ) ;
#2930=ADVANCED_FACE ( 'NONE', ( #45008 ), #41907, .T. ) ;
#2933=VERTEX_POINT ( 'NONE', #21043 ) ;
#2940=CARTESIAN_POINT ( 'NONE',  ( 96.46827370896536991, -25.18754255092518335, -13.99861390895580371 ) ) ;
#2950=CIRCLE ( 'NONE', #27705, 6.426280380454326924 ) ;
#2957=VERTEX_POINT ( 'NONE', #27677 ) ;
#2962=DIRECTION ( 'NONE',  ( 1.000000000000000000, 0.000000000000000000, -0.000000000000000000 ) ) ;
#2988=AXIS2_PLACEMENT_3D ( 'NONE', #4919, #40265, #19061 ) ;
#3000=EDGE_CURVE ( 'NONE', #32925, #14305, #16142, .T. ) ;
#3016=AXIS2_PLACEMENT_3D ( 'NONE', #22812, #36707, #22145 ) ;
#3043=ORIENTED_EDGE ( 'NONE', *, *, #16129, .T. ) ;
#3048=ORIENTED_EDGE ( 'NONE', *, *, #22274, .F. ) ;
#3053=DIRECTION ( 'NONE',  ( 0.000000000000000000, -0.3818493186865936084, 0.9242245927363024194 ) ) ;
#3060=CARTESIAN_POINT ( 'NONE',  ( 83.83554121260367253, -26.75858941326842810, -11.54476601486570964 ) ) ;
#3062=EDGE_CURVE ( 'NONE', #38783, #36515, #18522, .T. ) ;
#3071=DIRECTION ( 'NONE',  ( 1.000000000000000000, 0.000000000000000000, -0.000000000000000000 ) ) ;
#3091=EDGE_CURVE ( 'NONE', #10499, #36439, #12770, .T. ) ;
#3102=CONICAL_SURFACE ( 'NONE', #33670, 1.610000000000000986, 0.9599310885968765916 ) ;
#3108=ORIENTED_EDGE ( 'NONE', *, *, #8673, .T. ) ;
#3118=EDGE_CURVE ( 'NONE', #31077, #16022, #33141, .T. ) ;
#3120=MECHANICAL_DESIGN_GEOMETRIC_PRESENTATION_REPRESENTATION('',(#32202),#1166);
#3145=DIRECTION ( 'NONE',  ( 0.000000000000000000, -0.9242245927363041957, -0.3818493186865896671 ) ) ;
#3168=ORIENTED_EDGE ( 'NONE', *, *, #11769, .T. ) ;
#3169=AXIS2_PLACEMENT_3D ( 'NONE', #18891, #42847, #28716 ) ;
#3171=CARTESIAN_POINT ( 'NONE',  ( 91.11246428952674137, -25.99489077589524300, -13.39321520033831625 ) ) ;
#3175=CARTESIAN_POINT ( 'NONE',  ( 91.38554522942851577, -25.38011337280982715, -14.88121679464376257 ) ) ;
#3212=ORIENTED_EDGE ( 'NONE', *, *, #14450, .T. ) ;
#3218=EDGE_LOOP ( 'NONE', ( #13058, #19724, #35343, #35662, #45141 ) ) ;
#3219=ORIENTED_EDGE ( 'NONE', *, *, #4676, .F. ) ;
#3224=AXIS2_PLACEMENT_3D ( 'NONE', #32148, #15503, #4559 ) ;
#3252=CIRCLE ( 'NONE', #16373, 2.000000000000000444 ) ;
#3253=ORIENTED_EDGE ( 'NONE', *, *, #13645, .F. ) ;
#3262=ORIENTED_EDGE ( 'NONE', *, *, #18240, .T. ) ;
#3268=FACE_OUTER_BOUND ( 'NONE', #20576, .T. ) ;
#3286=ORIENTED_EDGE ( 'NONE', *, *, #42664, .F. ) ;
#3287=LINE ( 'NONE', #6943, #24417 ) ;
#3301=CARTESIAN_POINT ( 'NONE',  ( 96.46827370896536991, -25.85028767034691199, -12.39451169347363546 ) ) ;
#3316=EDGE_LOOP ( 'NONE', ( #20362, #18445, #22955, #37207, #34104 ) ) ;
#3318=VECTOR ( 'NONE', #5118, 999.9999999999998863 ) ;
#3324=ORIENTED_EDGE ( 'NONE', *, *, #35176, .T. ) ;
#3332=ORIENTED_EDGE ( 'NONE', *, *, #1737, .F. ) ;
#3347=VECTOR ( 'NONE', #35792, 1000.000000000000114 ) ;
#3385=CARTESIAN_POINT ( 'NONE',  ( 89.78938736644981589, -24.14644159042263993, -12.62951656296512937 ) ) ;
#3403=CONICAL_SURFACE ( 'NONE', #35405, 2.000000000000000444, 0.9599310885968830309 ) ;
#3420=DIRECTION ( 'NONE',  ( 0.000000000000000000, -0.3818493186865927203, 0.9242245927363029745 ) ) ;
#3424=ORIENTED_EDGE ( 'NONE', *, *, #6923, .T. ) ;
#3429=CARTESIAN_POINT ( 'NONE',  ( 84.38170309240724976, -25.99489077589524300, -13.39321520033831447 ) ) ;
#3446=VERTEX_POINT ( 'NONE', #10631 ) ;
#3459=CARTESIAN_POINT ( 'NONE',  ( 83.83554121260367253, -25.23119213852205789, -15.24166438581092109 ) ) ;
#3466=EDGE_CURVE ( 'NONE', #12518, #26941, #44871, .T. ) ;
#3473=DIRECTION ( 'NONE',  ( 1.000000000000000000, 0.000000000000000000, -0.000000000000000000 ) ) ;
#3480=ORIENTED_EDGE ( 'NONE', *, *, #31833, .F. ) ;
#3491=FACE_OUTER_BOUND ( 'NONE', #28535, .T. ) ;
#3494=DIRECTION ( 'NONE',  ( -1.224775218828351615E-16, 0.3818493186865896116, -0.9242245927363041957 ) ) ;
#3500=ORIENTED_EDGE ( 'NONE', *, *, #35952, .F. ) ;
#3529=CARTESIAN_POINT ( 'NONE',  ( 83.72016463086879412, -25.99489077589524300, -13.39321520033831447 ) ) ;
#3542=VERTEX_POINT ( 'NONE', #20895 ) ;
#3556=EDGE_CURVE ( 'NONE', #26284, #42482, #31021, .T. ) ;
#3564=CARTESIAN_POINT ( 'NONE',  ( 87.02785693856107230, -27.84333996136784961, -14.15691383771150136 ) ) ;
#3588=EDGE_CURVE ( 'NONE', #33401, #14434, #4777, .T. ) ;
#3612=EDGE_CURVE ( 'NONE', #14619, #21831, #36833, .T. ) ;
#3625=AXIS2_PLACEMENT_3D ( 'NONE', #11633, #18703, #11864 ) ;
#3628=ORIENTED_EDGE ( 'NONE', *, *, #21656, .F. ) ;
#3652=ORIENTED_EDGE ( 'NONE', *, *, #782, .T. ) ;
#3694=DIRECTION ( 'NONE',  ( 1.000000000000000000, 0.000000000000000000, -0.000000000000000000 ) ) ;
#3711=ORIENTED_EDGE ( 'NONE', *, *, #31833, .T. ) ;
#3712=CONICAL_SURFACE ( 'NONE', #8797, 2.000000000000000444, 0.9599310885968830309 ) ;
#3726=ORIENTED_EDGE ( 'NONE', *, *, #16414, .F. ) ;
#3780=VERTEX_POINT ( 'NONE', #1467 ) ;
#3798=CARTESIAN_POINT ( 'NONE',  ( 85.15861813568058380, -25.99489077589524300, -13.39321520033831625 ) ) ;
#3814=CARTESIAN_POINT ( 'NONE',  ( 90.33554924625337890, -25.99489077589524300, -13.39321520033831447 ) ) ;
#3815=ORIENTED_EDGE ( 'NONE', *, *, #9904, .T. ) ;
#3819=EDGE_LOOP ( 'NONE', ( #32133, #14848, #36999, #40879, #37690 ) ) ;
#3843=CIRCLE ( 'NONE', #32231, 2.000000000000000444 ) ;
#3867=ORIENTED_EDGE ( 'NONE', *, *, #13949, .T. ) ;
#3870=CARTESIAN_POINT ( 'NONE',  ( 89.40092984481313465, -25.38011337280982715, -14.88121679464376257 ) ) ;
#3871=AXIS2_PLACEMENT_3D ( 'NONE', #2838, #11209, #18039 ) ;
#3885=EDGE_CURVE ( 'NONE', #35058, #35857, #34500, .T. ) ;
#3894=CARTESIAN_POINT ( 'NONE',  ( 96.46827370896536991, -26.99359428275991846, -13.24861209478998170 ) ) ;
#3896=ORIENTED_EDGE ( 'NONE', *, *, #41842, .T. ) ;
#3927=DIRECTION ( 'NONE',  ( 0.000000000000000000, -0.3818493186865936084, 0.9242245927363024194 ) ) ;
#3935=ORIENTED_EDGE ( 'NONE', *, *, #28523, .F. ) ;
#3961=CARTESIAN_POINT ( 'NONE',  ( 85.43169907558235820, -25.99489077589524300, -13.39321520033831625 ) ) ;
#3965=ORIENTED_EDGE ( 'NONE', *, *, #19438, .T. ) ;
#3966=DIRECTION ( 'NONE',  ( -0.8949343913984424415, 0.4123869368673878100, 0.1703803081152053811 ) ) ;
#3993=ADVANCED_FACE ( 'NONE', ( #37715 ), #20176, .F. ) ;
#4002=CARTESIAN_POINT ( 'NONE',  ( 89.01247232317646763, -25.99489077589524300, -13.39321520033831447 ) ) ;
#4015=VECTOR ( 'NONE', #28408, 1000.000000000000114 ) ;
#4037=VECTOR ( 'NONE', #12912, 1000.000000000000114 ) ;
#4038=CARTESIAN_POINT ( 'NONE',  ( 86.09323753712084226, -25.99489077589524300, -13.39321520033831625 ) ) ;
#4039=ORIENTED_EDGE ( 'NONE', *, *, #43948, .F. ) ;
#4047=CARTESIAN_POINT ( 'NONE',  ( 93.44708369096697709, -25.99489077589524300, -13.39321520033831447 ) ) ;
#4057=DIRECTION ( 'NONE',  ( 1.000000000000000000, 0.000000000000000000, -0.000000000000000000 ) ) ;
#4068=DIRECTION ( 'NONE',  ( -0.5735764363510446051, 0.3127926500124816878, -0.7570804645221042017 ) ) ;
#4070=CARTESIAN_POINT ( 'NONE',  ( 91.11246428952674137, -25.23119213852205789, -15.24166438581092109 ) ) ;
#4074=CIRCLE ( 'NONE', #2651, 2.000000000000000444 ) ;
#4093=ORIENTED_EDGE ( 'NONE', *, *, #21558, .F. ) ;
#4113=CARTESIAN_POINT ( 'NONE',  ( 94.99177781699742695, -22.29799240495002977, -11.86581792559194426 ) ) ;
#4118=ORIENTED_EDGE ( 'NONE', *, *, #37835, .T. ) ;
#4121=DIRECTION ( 'NONE',  ( 0.000000000000000000, 0.9242245927363028635, 0.3818493186865930533 ) ) ;
#4136=EDGE_CURVE ( 'NONE', #33593, #9155, #44117, .T. ) ;
#4156=ORIENTED_EDGE ( 'NONE', *, *, #3556, .T. ) ;
#4162=VERTEX_POINT ( 'NONE', #4168 ) ;
#4168=CARTESIAN_POINT ( 'NONE',  ( 94.20708369096698220, -25.20837564747665027, -13.06826143013602604 ) ) ;
#4182=ORIENTED_EDGE ( 'NONE', *, *, #40198, .F. ) ;
#4184=DIRECTION ( 'NONE',  ( 0.5735764363510498232, -0.3127926500124802445, 0.7570804645221007600 ) ) ;
#4188=AXIS2_PLACEMENT_3D ( 'NONE', #32929, #4675, #43219 ) ;
#4213=EDGE_CURVE ( 'NONE', #42171, #40139, #32205, .T. ) ;
#4229=LINE ( 'NONE', #41881, #14315 ) ;
#4232=CONICAL_SURFACE ( 'NONE', #26839, 2.000000000000000444, 0.9599310885968830309 ) ;
#4235=ORIENTED_EDGE ( 'NONE', *, *, #35056, .T. ) ;
#4250=CARTESIAN_POINT ( 'NONE',  ( 88.73939138327467901, -25.38011337280982715, -14.88121679464376257 ) ) ;
#4274=ADVANCED_FACE ( 'NONE', ( #7143 ), #44904, .T. ) ;
#4289=ORIENTED_EDGE ( 'NONE', *, *, #1356, .F. ) ;
#4298=AXIS2_PLACEMENT_3D ( 'NONE', #44140, #45035, #6036 ) ;
#4318=VERTEX_POINT ( 'NONE', #7364 ) ;
#4346=EDGE_LOOP ( 'NONE', ( #28342, #5057, #32867, #3965 ) ) ;
#4353=VERTEX_POINT ( 'NONE', #35621 ) ;
#4367=CIRCLE ( 'NONE', #41531, 2.000000000000000444 ) ;
#4377=CARTESIAN_POINT ( 'NONE',  ( 85.04324155394569118, -25.99489077589524300, -13.39321520033831447 ) ) ;
#4397=CIRCLE ( 'NONE', #38627, 2.000000000000000444 ) ;
#4406=ORIENTED_EDGE ( 'NONE', *, *, #27344, .F. ) ;
#4442=CIRCLE ( 'NONE', #31386, 2.000000000000000444 ) ;
#4459=CIRCLE ( 'NONE', #41630, 0.8509999999999994236 ) ;
#4504=AXIS2_PLACEMENT_3D ( 'NONE', #15233, #4057, #17757 ) ;
#4511=CARTESIAN_POINT ( 'NONE',  ( 121.9470836909669913, -25.99489077589524300, -13.39321520033831447 ) ) ;
#4526=DIRECTION ( 'NONE',  ( 0.5735764363510498232, -0.3127926500124802445, 0.7570804645221007600 ) ) ;
#4527=AXIS2_PLACEMENT_3D ( 'NONE', #9186, #13288, #12842 ) ;
#4533=CARTESIAN_POINT ( 'NONE',  ( 94.20708369096698220, -25.89439488952623591, -12.28775498424876211 ) ) ;
#4535=ORIENTED_EDGE ( 'NONE', *, *, #21109, .F. ) ;
#4541=CARTESIAN_POINT ( 'NONE',  ( 91.11246428952674137, -25.99489077589524300, -13.39321520033831625 ) ) ;
#4544=VERTEX_POINT ( 'NONE', #39729 ) ;
#4551=VECTOR ( 'NONE', #42634, 1000.000000000000114 ) ;
#4556=DIRECTION ( 'NONE',  ( -0.5735764363510446051, 0.3127926500124816878, -0.7570804645221042017 ) ) ;
#4559=DIRECTION ( 'NONE',  ( 0.000000000000000000, -0.3818493186865927203, 0.9242245927363029745 ) ) ;
#4581=DIRECTION ( 'NONE',  ( -0.000000000000000000, -0.3818493186865928313, 0.9242245927363027524 ) ) ;
#4594=DIRECTION ( 'NONE',  ( 0.000000000000000000, -0.3818493186865927203, 0.9242245927363029745 ) ) ;
#4609=ORIENTED_EDGE ( 'NONE', *, *, #19759, .T. ) ;
#4624=ORIENTED_EDGE ( 'NONE', *, *, #44819, .F. ) ;
#4628=CARTESIAN_POINT ( 'NONE',  ( 85.43169907558235820, -25.99489077589524300, -13.39321520033831625 ) ) ;
#4641=CARTESIAN_POINT ( 'NONE',  ( 92.32016463086877422, -24.14644159042263993, -12.62951656296512937 ) ) ;
#4648=CARTESIAN_POINT ( 'NONE',  ( 121.9470836909669913, -25.99489077589524300, -13.39321520033831447 ) ) ;
#4651=ORIENTED_EDGE ( 'NONE', *, *, #11207, .T. ) ;
#4659=ADVANCED_FACE ( 'NONE', ( #8717 ), #24477, .T. ) ;
#4675=DIRECTION ( 'NONE',  ( -1.000000000000000000, 0.000000000000000000, 0.000000000000000000 ) ) ;
#4676=EDGE_CURVE ( 'NONE', #31533, #14596, #43154, .T. ) ;
#4690=EDGE_CURVE ( 'NONE', #8497, #14657, #20835, .T. ) ;
#4710=AXIS2_PLACEMENT_3D ( 'NONE', #41168, #13788, #37727 ) ;
#4726=ORIENTED_EDGE ( 'NONE', *, *, #18366, .F. ) ;
#4736=DIRECTION ( 'NONE',  ( 1.000000000000000000, 0.000000000000000000, -0.000000000000000000 ) ) ;
#4742=CONICAL_SURFACE ( 'NONE', #14941, 1.610000000000000986, 0.9599310885968765916 ) ;
#4770=LINE ( 'NONE', #15045, #37993 ) ;
#4777=CIRCLE ( 'NONE', #41931, 2.000000000000000444 ) ;
#4797=CARTESIAN_POINT ( 'NONE',  ( 96.46827370896536991, -25.99489077589524300, -13.39321520033831447 ) ) ;
#4798=CIRCLE ( 'NONE', #14278, 2.000000000000000444 ) ;
#4803=ORIENTED_EDGE ( 'NONE', *, *, #24252, .T. ) ;
#4813=ORIENTED_EDGE ( 'NONE', *, *, #43220, .T. ) ;
#4814=CYLINDRICAL_SURFACE ( 'NONE', #5541, 1.999999999999998890 ) ;
#4827=EDGE_LOOP ( 'NONE', ( #9468, #44057, #16669, #18786, #23239 ) ) ;
#4856=DIRECTION ( 'NONE',  ( 0.000000000000000000, -0.3818493186865936084, 0.9242245927363024194 ) ) ;
#4857=FACE_OUTER_BOUND ( 'NONE', #6650, .T. ) ;
#4865=DIRECTION ( 'NONE',  ( -0.5735764363510446051, 0.3127926500124816878, -0.7570804645221042017 ) ) ;
#4867=CARTESIAN_POINT ( 'NONE',  ( 91.38554522942851577, -25.99489077589524300, -13.39321520033831625 ) ) ;
#4868=CIRCLE ( 'NONE', #32525, 1.610000000000000986 ) ;
#4876=CARTESIAN_POINT ( 'NONE',  ( 88.35093386163799778, -24.14644159042263993, -12.62951656296512937 ) ) ;
#4893=CARTESIAN_POINT ( 'NONE',  ( 94.20708369096698220, -26.09538666226425363, -14.49867541642786861 ) ) ;
#4896=CARTESIAN_POINT ( 'NONE',  ( 90.99708770779186295, -25.23119213852205789, -15.24166438581092109 ) ) ;
#4899=AXIS2_PLACEMENT_3D ( 'NONE', #36805, #11758, #11987 ) ;
#4902=LINE ( 'NONE', #15174, #8580 ) ;
#4918=FACE_OUTER_BOUND ( 'NONE', #3819, .T. ) ;
#4919=CARTESIAN_POINT ( 'NONE',  ( 96.54708369096698561, -24.69793907545987466, -15.18364567559777178 ) ) ;
#4923=CARTESIAN_POINT ( 'NONE',  ( 93.44708369096697709, -22.29799240495002977, -11.86581792559194426 ) ) ;
#4929=DIRECTION ( 'NONE',  ( 0.000000000000000000, 0.3818493186865927203, -0.9242245927363029745 ) ) ;
#4941=DIRECTION ( 'NONE',  ( 0.000000000000000000, -0.3818493186865927203, 0.9242245927363029745 ) ) ;
#4988=SURFACE_STYLE_FILL_AREA ( #895 ) ;
#4989=CARTESIAN_POINT ( 'NONE',  ( 90.72400676789006013, -25.38011337280982715, -14.88121679464376257 ) ) ;
#5000=EDGE_CURVE ( 'NONE', #25709, #35629, #41968, .T. ) ;
#5002=ORIENTED_EDGE ( 'NONE', *, *, #8299, .F. ) ;
#5004=CARTESIAN_POINT ( 'NONE',  ( 90.06246830635160450, -25.99489077589524300, -13.39321520033831625 ) ) ;
#5006=DIRECTION ( 'NONE',  ( -1.000000000000000000, 0.000000000000000000, 0.000000000000000000 ) ) ;
#5009=CARTESIAN_POINT ( 'NONE',  ( 86.36631847702263087, -25.99489077589524300, -13.39321520033831447 ) ) ;
#5010=CIRCLE ( 'NONE', #2842, 1.610000000000000986 ) ;
#5028=ORIENTED_EDGE ( 'NONE', *, *, #4213, .T. ) ;
#5042=CARTESIAN_POINT ( 'NONE',  ( 90.45092582798827152, -25.99489077589524300, -13.39321520033831625 ) ) ;
#5043=DIRECTION ( 'NONE',  ( 0.000000000000000000, -0.3818493186865929978, 0.9242245927363029745 ) ) ;
#5052=AXIS2_PLACEMENT_3D ( 'NONE', #32669, #15359, #18998 ) ;
#5053=FACE_OUTER_BOUND ( 'NONE', #30142, .T. ) ;
#5057=ORIENTED_EDGE ( 'NONE', *, *, #16967, .T. ) ;
#5058=VERTEX_POINT ( 'NONE', #43775 ) ;
#5078=AXIS2_PLACEMENT_3D ( 'NONE', #10710, #38277, #24831 ) ;
#5088=ORIENTED_EDGE ( 'NONE', *, *, #19492, .F. ) ;
#5105=ORIENTED_EDGE ( 'NONE', *, *, #17516, .T. ) ;
#5118=DIRECTION ( 'NONE',  ( -0.000000000000000000, 0.9242245927363027524, 0.3818493186865931643 ) ) ;
#5144=DIRECTION ( 'NONE',  ( -1.000000000000000000, 0.000000000000000000, 0.000000000000000000 ) ) ;
#5153=CARTESIAN_POINT ( 'NONE',  ( 87.14323352029596492, -25.99489077589524300, -13.39321520033831625 ) ) ;
#5156=AXIS2_PLACEMENT_3D ( 'NONE', #6284, #37744, #27718 ) ;
#5170=CARTESIAN_POINT ( 'NONE',  ( 96.54708369096698561, -24.69793907545987466, -15.18364567559777178 ) ) ;
#5172=CIRCLE ( 'NONE', #8092, 1.610000000000000986 ) ;
#5195=CARTESIAN_POINT ( 'NONE',  ( 121.9470836909669913, -25.99489077589524300, -13.39321520033831447 ) ) ;
#5204=ADVANCED_FACE ( 'NONE', ( #43094 ), #37629, .T. ) ;
#5212=SHAPE_REPRESENTATION_RELATIONSHIP ( 'NONE' , 'NONE' ,  #850, #15621 ) ;
#5215=DIRECTION ( 'NONE',  ( 1.000000000000000000, 0.000000000000000000, -0.000000000000000000 ) ) ;
#5220=CARTESIAN_POINT ( 'NONE',  ( 84.10862215250544693, -26.60966817898065884, -11.90521360603286816 ) ) ;
#5224=EDGE_CURVE ( 'NONE', #25522, #39963, #16521, .T. ) ;
#5225=EDGE_CURVE ( 'NONE', #44907, #3542, #22786, .T. ) ;
#5232=CARTESIAN_POINT ( 'NONE',  ( 121.9470836909669913, -27.84333996136784961, -14.15691383771150136 ) ) ;
#5236=DIRECTION ( 'NONE',  ( 1.000000000000000000, 0.000000000000000000, -0.000000000000000000 ) ) ;
#5243=CARTESIAN_POINT ( 'NONE',  ( 88.46631044337289040, -25.99489077589524300, -13.39321520033831625 ) ) ;
#5258=EDGE_CURVE ( 'NONE', #22202, #7697, #8496, .T. ) ;
#5274=VECTOR ( 'NONE', #41527, 1000.000000000000227 ) ;
#5287=ORIENTED_EDGE ( 'NONE', *, *, #1737, .T. ) ;
#5289=ORIENTED_EDGE ( 'NONE', *, *, #16411, .F. ) ;
#5313=CARTESIAN_POINT ( 'NONE',  ( 88.46631044337289040, -24.14644159042263993, -12.62951656296512937 ) ) ;
#5335=B_SPLINE_CURVE_WITH_KNOTS ( 'NONE', 3,
 ( #32284, #25001, #35696, #379 ),
 .UNSPECIFIED., .F., .F.,
 ( 4, 4 ),
 ( 0.000000000000000000, 1.000000000000000000 ),
 .UNSPECIFIED. ) ;
#5338=CARTESIAN_POINT ( 'NONE',  ( 91.11246428952674137, -25.99489077589524300, -13.39321520033831625 ) ) ;
#5345=CARTESIAN_POINT ( 'NONE',  ( 89.40092984481313465, -26.60966817898065884, -11.90521360603286816 ) ) ;
#5349=CONICAL_SURFACE ( 'NONE', #9004, 1.610000000000000986, 0.9599310885968765916 ) ;
#5359=DIRECTION ( 'NONE',  ( 0.000000000000000000, -0.9242245927363028635, -0.3818493186865930533 ) ) ;
#5362=CARTESIAN_POINT ( 'NONE',  ( 94.20708369096698220, -26.42437990495228917, -14.12788525418686270 ) ) ;
#5370=AXIS2_PLACEMENT_3D ( 'NONE', #21196, #35073, #24841 ) ;
#5386=DIRECTION ( 'NONE',  ( 0.000000000000000000, -0.9242245927363029745, -0.3818493186865929978 ) ) ;
#5397=CARTESIAN_POINT ( 'NONE',  ( 90.45092582798827152, -24.14644159042263993, -12.62951656296512937 ) ) ;
#5411=EDGE_CURVE ( 'NONE', #20823, #24368, #45125, .T. ) ;
#5415=ORIENTED_EDGE ( 'NONE', *, *, #15561, .F. ) ;
#5424=DIRECTION ( 'NONE',  ( 0.000000000000000000, 0.3818493186865927203, -0.9242245927363029745 ) ) ;
#5426=DIRECTION ( 'NONE',  ( 0.000000000000000000, -0.3818493186865927203, 0.9242245927363029745 ) ) ;
#5448=VERTEX_POINT ( 'NONE', #2940 ) ;
#5472=ORIENTED_EDGE ( 'NONE', *, *, #37008, .T. ) ;
#5482=ORIENTED_EDGE ( 'NONE', *, *, #3588, .T. ) ;
#5491=ORIENTED_EDGE ( 'NONE', *, *, #35754, .T. ) ;
#5495=VERTEX_POINT ( 'NONE', #2712 ) ;
#5500=EDGE_CURVE ( 'NONE', #36439, #7248, #13445, .T. ) ;
#5502=ORIENTED_EDGE ( 'NONE', *, *, #2742, .T. ) ;
#5517=VERTEX_POINT ( 'NONE', #31203 ) ;
#5526=VERTEX_POINT ( 'NONE', #34609 ) ;
#5533=EDGE_CURVE ( 'NONE', #10907, #22858, #17264, .T. ) ;
#5541=AXIS2_PLACEMENT_3D ( 'NONE', #18284, #7567, #10778 ) ;
#5557=AXIS2_PLACEMENT_3D ( 'NONE', #16641, #22622, #25606 ) ;
#5572=DIRECTION ( 'NONE',  ( 0.5735764363510498232, -0.3127926500124802445, 0.7570804645221007600 ) ) ;
#5585=VECTOR ( 'NONE', #23015, 1000.000000000000227 ) ;
#5601=ORIENTED_EDGE ( 'NONE', *, *, #10985, .T. ) ;
#5610=CIRCLE ( 'NONE', #19454, 2.000000000000000444 ) ;
#5614=DIRECTION ( 'NONE',  ( 1.000000000000000000, 0.000000000000000000, -0.000000000000000000 ) ) ;
#5616=VECTOR ( 'NONE', #33420, 1000.000000000000000 ) ;
#5623=DIRECTION ( 'NONE',  ( 1.000000000000000000, 0.000000000000000000, -0.000000000000000000 ) ) ;
#5629=AXIS2_PLACEMENT_3D ( 'NONE', #31599, #592, #42326 ) ;
#5633=ORIENTED_EDGE ( 'NONE', *, *, #8889, .F. ) ;
#5642=FACE_OUTER_BOUND ( 'NONE', #15688, .T. ) ;
#5645=EDGE_CURVE ( 'NONE', #11206, #31913, #30339, .T. ) ;
#5655=CARTESIAN_POINT ( 'NONE',  ( 84.49707967414211396, -27.84333996136784961, -14.15691383771150136 ) ) ;
#5665=VECTOR ( 'NONE', #35917, 1000.000000000000000 ) ;
#5668=CARTESIAN_POINT ( 'NONE',  ( 86.75477599865929790, -25.99489077589524300, -13.39321520033831625 ) ) ;
#5669=ORIENTED_EDGE ( 'NONE', *, *, #16988, .F. ) ;
#5674=EDGE_LOOP ( 'NONE', ( #31624, #17050, #3212, #38793, #42386, #13562, #29152 ) ) ;
#5721=ORIENTED_EDGE ( 'NONE', *, *, #22277, .T. ) ;
#5757=ADVANCED_FACE ( 'NONE', ( #34389 ), #22331, .T. ) ;
#5785=EDGE_CURVE ( 'NONE', #26941, #12518, #36144, .T. ) ;
#5795=ORIENTED_EDGE ( 'NONE', *, *, #4690, .F. ) ;
#5805=VERTEX_POINT ( 'NONE', #24811 ) ;
#5806=VECTOR ( 'NONE', #23882, 1000.000000000000000 ) ;
#5816=CARTESIAN_POINT ( 'NONE',  ( 90.33554924625337890, -24.14644159042263993, -12.62951656296512937 ) ) ;
#5843=EDGE_CURVE ( 'NONE', #9192, #28442, #20904, .T. ) ;
#5850=FACE_OUTER_BOUND ( 'NONE', #13015, .T. ) ;
#5852=DIRECTION ( 'NONE',  ( 0.000000000000000000, -0.9242245927363029745, -0.3818493186865927758 ) ) ;
#5853=CIRCLE ( 'NONE', #35701, 2.000000000000000444 ) ;
#5901=AXIS2_PLACEMENT_3D ( 'NONE', #3429, #24187, #41525 ) ;
#5923=FACE_OUTER_BOUND ( 'NONE', #16201, .T. ) ;
#5936=ORIENTED_EDGE ( 'NONE', *, *, #21941, .T. ) ;
#5960=DIRECTION ( 'NONE',  ( -1.224775218828352108E-16, 0.9242245927363028635, 0.3818493186865928313 ) ) ;
#5983=CARTESIAN_POINT ( 'NONE',  ( 83.44708369096697709, -25.99489077589524300, -13.39321520033831625 ) ) ;
#5992=DIRECTION ( 'NONE',  ( -0.8949343913984423304, 0.1703803081152067689, -0.4123869368673877545 ) ) ;
#6002=EDGE_LOOP ( 'NONE', ( #30080, #44932, #35837, #33008, #14618 ) ) ;
#6019=CIRCLE ( 'NONE', #35137, 1.610000000000000986 ) ;
#6036=DIRECTION ( 'NONE',  ( 0.000000000000000000, -0.3818493186865927203, 0.9242245927363029745 ) ) ;
#6050=CARTESIAN_POINT ( 'NONE',  ( 91.77400275106518279, -25.23119213852205789, -15.24166438581092109 ) ) ;
#6100=CARTESIAN_POINT ( 'NONE',  ( 90.04708369096697140, -26.19154317501883611, -12.91723953507911915 ) ) ;
#6130=EDGE_LOOP ( 'NONE', ( #34269, #15670, #30579, #3332 ) ) ;
#6155=EDGE_LOOP ( 'NONE', ( #31973, #17966, #43756, #14319 ) ) ;
#6178=EDGE_CURVE ( 'NONE', #13605, #2957, #41436, .T. ) ;
#6193=ORIENTED_EDGE ( 'NONE', *, *, #24193, .T. ) ;
#6194=ORIENTED_EDGE ( 'NONE', *, *, #10583, .T. ) ;
#6228=ORIENTED_EDGE ( 'NONE', *, *, #16934, .F. ) ;
#6229=DIRECTION ( 'NONE',  ( 1.000000000000000000, 0.000000000000000000, -0.000000000000000000 ) ) ;
#6259=CARTESIAN_POINT ( 'NONE',  ( 94.20708369096698220, -25.99489077589524300, -13.39321520033831447 ) ) ;
#6270=DIRECTION ( 'NONE',  ( -1.000000000000000000, 0.000000000000000000, 0.000000000000000000 ) ) ;
#6284=CARTESIAN_POINT ( 'NONE',  ( 88.73939138327467901, -25.99489077589524300, -13.39321520033831625 ) ) ;
#6299=ORIENTED_EDGE ( 'NONE', *, *, #9249, .F. ) ;
#6315=EDGE_CURVE ( 'NONE', #30207, #26522, #15827, .T. ) ;
#6316=CYLINDRICAL_SURFACE ( 'NONE', #37492, 1.999999999999998890 ) ;
#6317=AXIS2_PLACEMENT_3D ( 'NONE', #3171, #27576, #41488 ) ;
#6327=CARTESIAN_POINT ( 'NONE',  ( 89.40092984481313465, -25.99489077589524300, -13.39321520033831625 ) ) ;
#6336=CARTESIAN_POINT ( 'NONE',  ( 84.49707967414211396, -25.99489077589524300, -13.39321520033831625 ) ) ;
#6351=CIRCLE ( 'NONE', #44927, 2.000000000000000444 ) ;
#6358=ADVANCED_FACE ( 'NONE', ( #43274 ), #24545, .T. ) ;
#6367=DIRECTION ( 'NONE',  ( -1.000000000000000000, 0.000000000000000000, 0.000000000000000000 ) ) ;
#6375=CARTESIAN_POINT ( 'NONE',  ( 93.24708369096698846, -24.14644159042263993, -12.62951656296512937 ) ) ;
#6390=ORIENTED_EDGE ( 'NONE', *, *, #41804, .T. ) ;
#6396=DIRECTION ( 'NONE',  ( 0.000000000000000000, -0.9242245927363029745, -0.3818493186865927758 ) ) ;
#6417=EDGE_CURVE ( 'NONE', #2957, #29689, #31818, .T. ) ;
#6475=DIRECTION ( 'NONE',  ( 1.000000000000000000, 0.000000000000000000, -0.000000000000000000 ) ) ;
#6476=ORIENTED_EDGE ( 'NONE', *, *, #25847, .F. ) ;
#6485=DIRECTION ( 'NONE',  ( 0.000000000000000000, 0.9242245927363027524, 0.3818493186865928868 ) ) ;
#6501=EDGE_LOOP ( 'NONE', ( #44323, #42058, #33960, #33933, #13218 ) ) ;
#6503=AXIS2_PLACEMENT_3D ( 'NONE', #30220, #34079, #40945 ) ;
#6511=DIRECTION ( 'NONE',  ( 1.000000000000000000, 0.000000000000000000, -0.000000000000000000 ) ) ;
#6527=ORIENTED_EDGE ( 'NONE', *, *, #34763, .F. ) ;
#6534=VECTOR ( 'NONE', #4526, 1000.000000000000114 ) ;
#6540=CIRCLE ( 'NONE', #25486, 1.610000000000000986 ) ;
#6553=DIRECTION ( 'NONE',  ( 1.000000000000000000, 0.000000000000000000, -0.000000000000000000 ) ) ;
#6562=DIRECTION ( 'NONE',  ( 1.000000000000000000, 0.000000000000000000, -0.000000000000000000 ) ) ;
#6565=ORIENTED_EDGE ( 'NONE', *, *, #28729, .F. ) ;
#6569=DIRECTION ( 'NONE',  ( 1.000000000000000000, 0.000000000000000000, -0.000000000000000000 ) ) ;
#6571=ORIENTED_EDGE ( 'NONE', *, *, #17851, .F. ) ;
#6593=CARTESIAN_POINT ( 'NONE',  ( 94.99177781699742695, -22.63071325833509917, -12.00328368031911630 ) ) ;
#6604=CONICAL_SURFACE ( 'NONE', #30632, 2.000000000000000444, 0.9599310885968830309 ) ;
#6625=PLANE ( 'NONE',  #1917 ) ;
#6628=AXIS2_PLACEMENT_3D ( 'NONE', #44419, #23215, #41454 ) ;
#6636=ORIENTED_EDGE ( 'NONE', *, *, #19032, .T. ) ;
#6638=EDGE_CURVE ( 'NONE', #18337, #22858, #26040, .T. ) ;
#6639=DIRECTION ( 'NONE',  ( 1.000000000000000000, 0.000000000000000000, -0.000000000000000000 ) ) ;
#6640=AXIS2_PLACEMENT_3D ( 'NONE', #38969, #31676, #14584 ) ;
#6650=EDGE_LOOP ( 'NONE', ( #15048, #28604, #9104, #28356, #1184, #24409 ) ) ;
#6659=CIRCLE ( 'NONE', #8827, 0.8509999999999994236 ) ;
#6672=CIRCLE ( 'NONE', #34323, 1.610000000000000986 ) ;
#6697=EDGE_LOOP ( 'NONE', ( #6565, #17462, #25426, #2406, #42704 ) ) ;
#6699=ADVANCED_FACE ( 'NONE', ( #43447 ), #23879, .F. ) ;
#6703=DIRECTION ( 'NONE',  ( 1.000000000000000000, 0.000000000000000000, -0.000000000000000000 ) ) ;
#6714=CARTESIAN_POINT ( 'NONE',  ( 91.11246428952674137, -25.99489077589524300, -13.39321520033831625 ) ) ;
#6724=VECTOR ( 'NONE', #41344, 1000.000000000000114 ) ;
#6751=ORIENTED_EDGE ( 'NONE', *, *, #21116, .T. ) ;
#6778=FACE_OUTER_BOUND ( 'NONE', #3218, .T. ) ;
#6805=EDGE_CURVE ( 'NONE', #42907, #17457, #31856, .T. ) ;
#6817=CARTESIAN_POINT ( 'NONE',  ( 91.77400275106518279, -25.99489077589524300, -13.39321520033831625 ) ) ;
#6823=ADVANCED_FACE ( 'NONE', ( #29532 ), #7846, .T. ) ;
#6828=CARTESIAN_POINT ( 'NONE',  ( 93.93057702947278642, -25.99489077589524300, -13.39321520033831447 ) ) ;
#6861=ORIENTED_EDGE ( 'NONE', *, *, #8696, .T. ) ;
#6866=LINE ( 'NONE', #20774, #22377 ) ;
#6891=DIRECTION ( 'NONE',  ( 1.000000000000000000, 0.000000000000000000, -0.000000000000000000 ) ) ;
#6901=CARTESIAN_POINT ( 'NONE',  ( 96.54708369096698561, -25.64989040597826175, -15.57695047384496156 ) ) ;
#6903=AXIS2_PLACEMENT_3D ( 'NONE', #22847, #5960, #9392 ) ;
#6922=EDGE_CURVE ( 'NONE', #15443, #28262, #37701, .T. ) ;
#6923=EDGE_CURVE ( 'NONE', #17457, #21347, #18024, .T. ) ;
#6930=ADVANCED_FACE ( 'NONE', ( #8561 ), #33376, .T. ) ;
#6936=EDGE_CURVE ( 'NONE', #37642, #19531, #9015, .T. ) ;
#6942=ORIENTED_EDGE ( 'NONE', *, *, #15899, .F. ) ;
#6943=CARTESIAN_POINT ( 'NONE',  ( 86.09323753712084226, -26.60966817898065884, -11.90521360603286816 ) ) ;
#6962=CARTESIAN_POINT ( 'NONE',  ( 86.48169505875749508, -25.99489077589524300, -13.39321520033831625 ) ) ;
#6969=ORIENTED_EDGE ( 'NONE', *, *, #39328, .T. ) ;
#7026=AXIS2_PLACEMENT_3D ( 'NONE', #2661, #17047, #9514 ) ;
#7057=DIRECTION ( 'NONE',  ( 1.000000000000000000, 0.000000000000000000, -0.000000000000000000 ) ) ;
#7067=EDGE_LOOP ( 'NONE', ( #28374, #837, #13477, #30475, #29245 ) ) ;
#7132=CARTESIAN_POINT ( 'NONE',  ( 85.43169907558235820, -25.99489077589524300, -13.39321520033831625 ) ) ;
#7137=EDGE_LOOP ( 'NONE', ( #29978, #27047, #17146, #43693, #27293, #42260 ) ) ;
#7143=FACE_OUTER_BOUND ( 'NONE', #4827, .T. ) ;
#7155=CARTESIAN_POINT ( 'NONE',  ( 96.46827370896536991, -25.85028767034691199, -12.39451169347363546 ) ) ;
#7222=DIRECTION ( 'NONE',  ( 1.000000000000000000, 0.000000000000000000, -0.000000000000000000 ) ) ;
#7233=VECTOR ( 'NONE', #22939, 1000.000000000000000 ) ;
#7238=ADVANCED_FACE ( 'NONE', ( #10377 ), #2616, .T. ) ;
#7243=EDGE_CURVE ( 'NONE', #13898, #29623, #22391, .T. ) ;
#7248=VERTEX_POINT ( 'NONE', #27258 ) ;
#7257=AXIS2_PLACEMENT_3D ( 'NONE', #32020, #31799, #42082 ) ;
#7281=ORIENTED_EDGE ( 'NONE', *, *, #18105, .F. ) ;
#7290=CARTESIAN_POINT ( 'NONE',  ( 88.73939138327467901, -25.99489077589524300, -13.39321520033831625 ) ) ;
#7293=CARTESIAN_POINT ( 'NONE',  ( 1093.930577029472943, -25.99489077589524300, -13.39321520033831447 ) ) ;
#7294=CIRCLE ( 'NONE', #8021, 1.610000000000000986 ) ;
#7332=FACE_OUTER_BOUND ( 'NONE', #29233, .T. ) ;
#7338=CONICAL_SURFACE ( 'NONE', #8770, 1.610000000000000986, 0.9599310885968765916 ) ;
#7351=FACE_OUTER_BOUND ( 'NONE', #8877, .T. ) ;
#7364=CARTESIAN_POINT ( 'NONE',  ( 86.36631847702263087, -26.75858941326842810, -11.54476601486570964 ) ) ;
#7400=ORIENTED_EDGE ( 'NONE', *, *, #37934, .T. ) ;
#7405=VERTEX_POINT ( 'NONE', #27030 ) ;
#7421=DIRECTION ( 'NONE',  ( -0.5735764363510450492, -0.3127926500124816878, 0.7570804645221038687 ) ) ;
#7437=FACE_OUTER_BOUND ( 'NONE', #31671, .T. ) ;
#7448=CARTESIAN_POINT ( 'NONE',  ( 92.04708369096698561, -25.99489077589524300, -13.39321520033831625 ) ) ;
#7460=DIRECTION ( 'NONE',  ( 0.000000000000000000, -0.3818493186865927203, 0.9242245927363029745 ) ) ;
#7461=ORIENTED_EDGE ( 'NONE', *, *, #45120, .T. ) ;
#7463=EDGE_CURVE ( 'NONE', #735, #12514, #14459, .T. ) ;
#7465=EDGE_CURVE ( 'NONE', #7697, #17646, #20380, .T. ) ;
#7474=CARTESIAN_POINT ( 'NONE',  ( 86.09323753712084226, -25.99489077589524300, -13.39321520033831625 ) ) ;
#7477=AXIS2_PLACEMENT_3D ( 'NONE', #38844, #14916, #35414 ) ;
#7485=EDGE_CURVE ( 'NONE', #30859, #16407, #20343, .T. ) ;
#7522=ORIENTED_EDGE ( 'NONE', *, *, #34241, .F. ) ;
#7536=DIRECTION ( 'NONE',  ( 0.000000000000000000, -0.3818493186865927203, 0.9242245927363029745 ) ) ;
#7545=EDGE_LOOP ( 'NONE', ( #6193, #32571 ) ) ;
#7567=DIRECTION ( 'NONE',  ( 1.000000000000000000, 0.000000000000000000, -0.000000000000000000 ) ) ;
#7574=ORIENTED_EDGE ( 'NONE', *, *, #14450, .F. ) ;
#7588=EDGE_CURVE ( 'NONE', #42171, #1522, #10599, .T. ) ;
#7600=VECTOR ( 'NONE', #43151, 1000.000000000000227 ) ;
#7603=DIRECTION ( 'NONE',  ( 1.000000000000000000, 0.000000000000000000, -0.000000000000000000 ) ) ;
#7658=ORIENTED_EDGE ( 'NONE', *, *, #5645, .T. ) ;
#7664=LINE ( 'NONE', #31610, #14009 ) ;
#7697=VERTEX_POINT ( 'NONE', #5313 ) ;
#7709=FACE_OUTER_BOUND ( 'NONE', #22621, .T. ) ;
#7716=VERTEX_POINT ( 'NONE', #29040 ) ;
#7719=EDGE_CURVE ( 'NONE', #11048, #41727, #35607, .T. ) ;
#7720=DIRECTION ( 'NONE',  ( 1.000000000000000000, 0.000000000000000000, -0.000000000000000000 ) ) ;
#7733=VERTEX_POINT ( 'NONE', #22867 ) ;
#7744=ORIENTED_EDGE ( 'NONE', *, *, #5224, .T. ) ;
#7754=EDGE_CURVE ( 'NONE', #12295, #21542, #36760, .T. ) ;
#7755=ADVANCED_FACE ( 'NONE', ( #29941 ), #29708, .F. ) ;
#7768=CARTESIAN_POINT ( 'NONE',  ( 96.46827370896536991, -25.38949206727775731, -12.58586697536825660 ) ) ;
#7778=AXIS2_PLACEMENT_3D ( 'NONE', #17746, #31642, #24593 ) ;
#7789=CARTESIAN_POINT ( 'NONE',  ( 96.23375075340858587, -25.23356801022904961, -15.23591384769724755 ) ) ;
#7790=LINE ( 'NONE', #25569, #40775 ) ;
#7801=AXIS2_PLACEMENT_3D ( 'NONE', #15103, #965, #1848 ) ;
#7807=CIRCLE ( 'NONE', #15814, 2.000000000000000444 ) ;
#7811=ORIENTED_EDGE ( 'NONE', *, *, #7243, .F. ) ;
#7815=AXIS2_PLACEMENT_3D ( 'NONE', #12270, #19325, #36858 ) ;
#7840=ORIENTED_EDGE ( 'NONE', *, *, #32648, .T. ) ;
#7842=CARTESIAN_POINT ( 'NONE',  ( 90.48265143217095385, -26.32847964148556485, -12.58579976615069818 ) ) ;
#7846=CONICAL_SURFACE ( 'NONE', #4188, 2.000000000000000444, 0.9599310885968830309 ) ;
#7857=DIRECTION ( 'NONE',  ( 0.000000000000000000, -0.9242245927363028635, -0.3818493186865930533 ) ) ;
#7868=EDGE_LOOP ( 'NONE', ( #22553, #20354, #32686, #29684, #6228 ) ) ;
#7878=DIRECTION ( 'NONE',  ( 0.5735764363510498232, -0.3127926500124802445, 0.7570804645221007600 ) ) ;
#7880=DIRECTION ( 'NONE',  ( 1.000000000000000000, 0.000000000000000000, -0.000000000000000000 ) ) ;
#7904=DIRECTION ( 'NONE',  ( 0.000000000000000000, -0.3818493186865927203, 0.9242245927363029745 ) ) ;
#7921=FACE_OUTER_BOUND ( 'NONE', #16008, .T. ) ;
#7931=CARTESIAN_POINT ( 'NONE',  ( 86.36631847702263087, -25.23119213852205789, -15.24166438581092109 ) ) ;
#7947=AXIS2_PLACEMENT_3D ( 'NONE', #21368, #619, #42355 ) ;
#7965=( LENGTH_UNIT ( ) NAMED_UNIT ( * ) SI_UNIT ( .MILLI., .METRE. ) );
#7970=FACE_OUTER_BOUND ( 'NONE', #16976, .T. ) ;
#7989=CIRCLE ( 'NONE', #24127, 2.000000000000000444 ) ;
#8021=AXIS2_PLACEMENT_3D ( 'NONE', #19169, #39694, #18722 ) ;
#8023=CARTESIAN_POINT ( 'NONE',  ( 121.9470836909669913, -25.99489077589524300, -13.39321520033831447 ) ) ;
#8031=ORIENTED_EDGE ( 'NONE', *, *, #8110, .F. ) ;
#8038=EDGE_CURVE ( 'NONE', #38783, #19531, #27631, .T. ) ;
#8043=DIRECTION ( 'NONE',  ( -0.5735764363510450492, -0.3127926500124816878, 0.7570804645221038687 ) ) ;
#8049=ADVANCED_FACE ( 'NONE', ( #23842 ), #17652, .T. ) ;
#8072=EDGE_CURVE ( 'NONE', #37642, #35430, #22535, .T. ) ;
#8073=ADVANCED_FACE ( 'NONE', ( #38382 ), #21065, .T. ) ;
#8077=DIRECTION ( 'NONE',  ( 1.000000000000000000, 0.000000000000000000, -0.000000000000000000 ) ) ;
#8078=ORIENTED_EDGE ( 'NONE', *, *, #41778, .F. ) ;
#8089=VERTEX_POINT ( 'NONE', #7155 ) ;
#8091=DIRECTION ( 'NONE',  ( 1.000000000000000000, 0.000000000000000000, -0.000000000000000000 ) ) ;
#8092=AXIS2_PLACEMENT_3D ( 'NONE', #36426, #1771, #1548 ) ;
#8097=CIRCLE ( 'NONE', #5901, 2.000000000000000444 ) ;
#8110=EDGE_CURVE ( 'NONE', #26941, #10499, #24282, .T. ) ;
#8154=DIRECTION ( 'NONE',  ( -1.000000000000000000, 0.000000000000000000, 0.000000000000000000 ) ) ;
#8178=FACE_OUTER_BOUND ( 'NONE', #39672, .T. ) ;
#8180=AXIS2_PLACEMENT_3D ( 'NONE', #6100, #33903, #30498 ) ;
#8184=ORIENTED_EDGE ( 'NONE', *, *, #40198, .T. ) ;
#8198=LINE ( 'NONE', #1123, #39744 ) ;
#8199=ORIENTED_EDGE ( 'NONE', *, *, #11652, .T. ) ;
#8201=ADVANCED_FACE ( 'NONE', ( #4857 ), #10814, .T. ) ;
#8213=DIRECTION ( 'NONE',  ( 1.000000000000000000, 0.000000000000000000, -0.000000000000000000 ) ) ;
#8256=CIRCLE ( 'NONE', #20634, 2.000000000000000444 ) ;
#8264=ORIENTED_EDGE ( 'NONE', *, *, #30047, .F. ) ;
#8271=VERTEX_POINT ( 'NONE', #38835 ) ;
#8290=ORIENTED_EDGE ( 'NONE', *, *, #15239, .F. ) ;
#8299=EDGE_CURVE ( 'NONE', #31941, #2957, #34875, .T. ) ;
#8317=ORIENTED_EDGE ( 'NONE', *, *, #11114, .T. ) ;
#8325=CARTESIAN_POINT ( 'NONE',  ( 121.9470836909669913, -25.99489077589524300, -13.39321520033831447 ) ) ;
#8356=CARTESIAN_POINT ( 'NONE',  ( 84.10862215250544693, -25.99489077589524300, -13.39321520033831625 ) ) ;
#8363=ORIENTED_EDGE ( 'NONE', *, *, #16395, .F. ) ;
#8377=EDGE_CURVE ( 'NONE', #7733, #39054, #44473, .T. ) ;
#8392=CIRCLE ( 'NONE', #33866, 1.999999999999998890 ) ;
#8393=CARTESIAN_POINT ( 'NONE',  ( 89.78938736644981589, -25.99489077589524300, -13.39321520033831625 ) ) ;
#8402=ORIENTED_EDGE ( 'NONE', *, *, #11933, .F. ) ;
#8406=DIRECTION ( 'NONE',  ( 0.000000000000000000, -0.3818493186865927203, 0.9242245927363029745 ) ) ;
#8410=VERTEX_POINT ( 'NONE', #37388 ) ;
#8438=EDGE_CURVE ( 'NONE', #16407, #24250, #23730, .T. ) ;
#8439=AXIS2_PLACEMENT_3D ( 'NONE', #21429, #18235, #31681 ) ;
#8443=CARTESIAN_POINT ( 'NONE',  ( 84.38170309240724976, -27.84333996136784961, -14.15691383771150136 ) ) ;
#8447=CONICAL_SURFACE ( 'NONE', #14271, 3077.683537175320453, 1.256637061435923686 ) ;
#8465=DIRECTION ( 'NONE',  ( 0.000000000000000000, -0.9242245927363028635, -0.3818493186865930533 ) ) ;
#8481=CIRCLE ( 'NONE', #28856, 2.000000000000000444 ) ;
#8496=CIRCLE ( 'NONE', #28172, 2.000000000000000444 ) ;
#8497=VERTEX_POINT ( 'NONE', #28486 ) ;
#8498=CARTESIAN_POINT ( 'NONE',  ( 83.83554121260367253, -26.75858941326842810, -11.54476601486570964 ) ) ;
#8545=VECTOR ( 'NONE', #10028, 1000.000000000000000 ) ;
#8561=FACE_OUTER_BOUND ( 'NONE', #44889, .T. ) ;
#8580=VECTOR ( 'NONE', #22463, 999.9999999999998863 ) ;
#8605=ADVANCED_FACE ( 'NONE', ( #28710 ), #17988, .T. ) ;
#8607=CARTESIAN_POINT ( 'NONE',  ( 91.11246428952674137, -25.99489077589524300, -13.39321520033831625 ) ) ;
#8652=EDGE_LOOP ( 'NONE', ( #17737, #4182, #20743, #6194, #39504 ) ) ;
#8657=ORIENTED_EDGE ( 'NONE', *, *, #34603, .T. ) ;
#8673=EDGE_CURVE ( 'NONE', #3446, #22843, #29729, .T. ) ;
#8695=LINE ( 'NONE', #22827, #15563 ) ;
#8696=EDGE_CURVE ( 'NONE', #43595, #31077, #32110, .T. ) ;
#8705=VECTOR ( 'NONE', #13012, 1000.000000000000000 ) ;
#8717=FACE_OUTER_BOUND ( 'NONE', #37955, .T. ) ;
#8731=AXIS2_PLACEMENT_3D ( 'NONE', #14846, #43333, #12102 ) ;
#8746=ADVANCED_FACE ( 'NONE', ( #1105 ), #10708, .T. ) ;
#8763=CONICAL_SURFACE ( 'NONE', #16061, 1.610000000000000986, 0.9599310885968765916 ) ;
#8770=AXIS2_PLACEMENT_3D ( 'NONE', #40267, #32948, #18837 ) ;
#8783=CARTESIAN_POINT ( 'NONE',  ( 86.09323753712084226, -25.99489077589524300, -13.39321520033831625 ) ) ;
#8795=FACE_OUTER_BOUND ( 'NONE', #5674, .T. ) ;
#8797=AXIS2_PLACEMENT_3D ( 'NONE', #36651, #29375, #5424 ) ;
#8827=AXIS2_PLACEMENT_3D ( 'NONE', #6259, #20403, #41157 ) ;
#8850=DIRECTION ( 'NONE',  ( 1.000000000000000000, 0.000000000000000000, -0.000000000000000000 ) ) ;
#8874=CONICAL_SURFACE ( 'NONE', #28540, 2.000000000000000444, 0.9599310885968830309 ) ;
#8877=EDGE_LOOP ( 'NONE', ( #20314, #22437, #2024, #21245 ) ) ;
#8889=EDGE_CURVE ( 'NONE', #2587, #22394, #10936, .T. ) ;
#8918=CARTESIAN_POINT ( 'NONE',  ( 94.20708369096698220, -27.10035099198479358, -13.29271931396930739 ) ) ;
#8919=VERTEX_POINT ( 'NONE', #4533 ) ;
#8925=DIRECTION ( 'NONE',  ( 1.000000000000000000, 0.000000000000000000, -0.000000000000000000 ) ) ;
#8931=AXIS2_PLACEMENT_3D ( 'NONE', #42108, #27979, #10869 ) ;
#8946=CARTESIAN_POINT ( 'NONE',  ( 83.83554121260367253, -27.84333996136784961, -14.15691383771150136 ) ) ;
#8952=EDGE_CURVE ( 'NONE', #40373, #29623, #14128, .T. ) ;
#8975=CONICAL_SURFACE ( 'NONE', #34406, 1.610000000000000986, 0.9599310885968765916 ) ;
#9004=AXIS2_PLACEMENT_3D ( 'NONE', #4038, #39613, #22283 ) ;
#9015=LINE ( 'NONE', #22913, #38390 ) ;
#9022=DIRECTION ( 'NONE',  ( 0.000000000000000000, 0.9242245927363040847, 0.3818493186865896671 ) ) ;
#9042=LINE ( 'NONE', #32956, #7233 ) ;
#9052=DIRECTION ( 'NONE',  ( 0.000000000000000000, -0.3818493186865936084, 0.9242245927363024194 ) ) ;
#9055=CIRCLE ( 'NONE', #3224, 2.000000000000000444 ) ;
#9081=VECTOR ( 'NONE', #24110, 1000.000000000000114 ) ;
#9090=ORIENTED_EDGE ( 'NONE', *, *, #9573, .T. ) ;
#9092=AXIS2_PLACEMENT_3D ( 'NONE', #12040, #37078, #5852 ) ;
#9094=ORIENTED_EDGE ( 'NONE', *, *, #44807, .F. ) ;
#9104=ORIENTED_EDGE ( 'NONE', *, *, #13069, .T. ) ;
#9110=ORIENTED_EDGE ( 'NONE', *, *, #2742, .F. ) ;
#9116=VECTOR ( 'NONE', #6475, 1000.000000000000000 ) ;
#9128=EDGE_LOOP ( 'NONE', ( #23639, #15600, #33915, #40784, #27439, #30548 ) ) ;
#9136=EDGE_LOOP ( 'NONE', ( #5669, #30467, #21637, #23005, #41024 ) ) ;
#9139=FACE_OUTER_BOUND ( 'NONE', #40245, .T. ) ;
#9151=ADVANCED_FACE ( 'NONE', ( #29156 ), #4232, .T. ) ;
#9155=VERTEX_POINT ( 'NONE', #36659 ) ;
#9158=VECTOR ( 'NONE', #13335, 1000.000000000000114 ) ;
#9174=AXIS2_PLACEMENT_3D ( 'NONE', #28750, #35564, #18709 ) ;
#9175=DIRECTION ( 'NONE',  ( -0.4461977533474357771, 0.3417300876246960328, -0.8271203734159368048 ) ) ;
#9186=CARTESIAN_POINT ( 'NONE',  ( 90.04708369096697140, -25.99489077589524300, -13.39321520033831447 ) ) ;
#9192=VERTEX_POINT ( 'NONE', #36436 ) ;
#9231=CIRCLE ( 'NONE', #15057, 1.610000000000000986 ) ;
#9232=PLANE ( 'NONE',  #24143 ) ;
#9249=EDGE_CURVE ( 'NONE', #42907, #37027, #33354, .T. ) ;
#9283=AXIS2_PLACEMENT_3D ( 'NONE', #30485, #44636, #9292 ) ;
#9286=DIRECTION ( 'NONE',  ( -1.000000000000000000, 0.000000000000000000, 0.000000000000000000 ) ) ;
#9292=DIRECTION ( 'NONE',  ( 0.000000000000000000, -0.3818493186865927203, 0.9242245927363029745 ) ) ;
#9317=ORIENTED_EDGE ( 'NONE', *, *, #32665, .F. ) ;
#9330=DIRECTION ( 'NONE',  ( 0.000000000000000000, -0.3818493186865936084, 0.9242245927363024194 ) ) ;
#9362=EDGE_LOOP ( 'NONE', ( #1393, #19446, #15235, #2423, #21861, #29572 ) ) ;
#9387=ORIENTED_EDGE ( 'NONE', *, *, #4676, .T. ) ;
#9392=DIRECTION ( 'NONE',  ( 1.000000000000000000, 1.131967377815149893E-16, 4.676795828538290169E-17 ) ) ;
#9405=LINE ( 'NONE', #16025, #32919 ) ;
#9418=DIRECTION ( 'NONE',  ( 1.000000000000000000, 0.000000000000000000, -0.000000000000000000 ) ) ;
#9421=CARTESIAN_POINT ( 'NONE',  ( 121.9470836909669913, -24.14644159042263993, -12.62951656296512937 ) ) ;
#9427=VECTOR ( 'NONE', #39972, 1000.000000000000114 ) ;
#9462=CIRCLE ( 'NONE', #21215, 2.000000000000000444 ) ;
#9468=ORIENTED_EDGE ( 'NONE', *, *, #8072, .F. ) ;
#9470=PLANE ( 'NONE',  #42821 ) ;
#9477=CARTESIAN_POINT ( 'NONE',  ( 89.67401078471493747, -25.23119213852205789, -15.24166438581092109 ) ) ;
#9491=CIRCLE ( 'NONE', #16029, 1.009117809157100254 ) ;
#9510=DIRECTION ( 'NONE',  ( 1.000000000000000000, 0.000000000000000000, -0.000000000000000000 ) ) ;
#9514=DIRECTION ( 'NONE',  ( 0.000000000000000000, -0.9242245927363029745, -0.3818493186865927203 ) ) ;
#9531=CIRCLE ( 'NONE', #17529, 2.000000000000000444 ) ;
#9563=AXIS2_PLACEMENT_3D ( 'NONE', #17482, #44869, #14065 ) ;
#9573=EDGE_CURVE ( 'NONE', #14657, #35146, #13085, .T. ) ;
#9582=VERTEX_POINT ( 'NONE', #17727 ) ;
#9599=VECTOR ( 'NONE', #28548, 1000.000000000000000 ) ;
#9623=FACE_OUTER_BOUND ( 'NONE', #21419, .T. ) ;
#9626=VECTOR ( 'NONE', #4068, 1000.000000000000114 ) ;
#9633=ORIENTED_EDGE ( 'NONE', *, *, #10295, .F. ) ;
#9636=CARTESIAN_POINT ( 'NONE',  ( 86.36631847702263087, -27.84333996136784961, -14.15691383771150136 ) ) ;
#9670=ORIENTED_EDGE ( 'NONE', *, *, #7465, .F. ) ;
#9693=CARTESIAN_POINT ( 'NONE',  ( 84.49707967414211396, -25.99489077589524300, -13.39321520033831625 ) ) ;
#9706=ADVANCED_FACE ( 'NONE', ( #38684 ), #26897, .T. ) ;
#9721=CIRCLE ( 'NONE', #230, 1.610000000000000986 ) ;
#9728=EDGE_CURVE ( 'NONE', #15657, #35973, #27629, .T. ) ;
#9741=CARTESIAN_POINT ( 'NONE',  ( 91.77400275106518279, -25.99489077589524300, -13.39321520033831625 ) ) ;
#9787=CIRCLE ( 'NONE', #10496, 2.000000000000000444 ) ;
#9792=ORIENTED_EDGE ( 'NONE', *, *, #28832, .T. ) ;
#9827=CARTESIAN_POINT ( 'NONE',  ( 95.28169473643895060, -25.99489077589524300, -13.39321520033831447 ) ) ;
#9833=CARTESIAN_POINT ( 'NONE',  ( 96.54708369096698561, -24.20446030063578391, -12.09626349990295147 ) ) ;
#9845=EDGE_CURVE ( 'NONE', #18037, #5517, #9042, .T. ) ;
#9869=ORIENTED_EDGE ( 'NONE', *, *, #19486, .F. ) ;
#9879=ORIENTED_EDGE ( 'NONE', *, *, #22523, .F. ) ;
#9900=ORIENTED_EDGE ( 'NONE', *, *, #37536, .T. ) ;
#9904=EDGE_CURVE ( 'NONE', #40373, #12976, #5010, .T. ) ;
#9908=AXIS2_PLACEMENT_3D ( 'NONE', #42434, #691, #32599 ) ;
#9916=DIRECTION ( 'NONE',  ( -1.000000000000000000, 0.000000000000000000, 0.000000000000000000 ) ) ;
#9929=VECTOR ( 'NONE', #3966, 1000.000000000000114 ) ;
#9931=VERTEX_POINT ( 'NONE', #43251 ) ;
#9937=CARTESIAN_POINT ( 'NONE',  ( 83.72016463086879412, -25.99489077589524300, -13.39321520033831447 ) ) ;
#9941=LINE ( 'NONE', #30451, #14343 ) ;
#9964=AXIS2_PLACEMENT_3D ( 'NONE', #42029, #3494, #24688 ) ;
#9971=CIRCLE ( 'NONE', #35416, 2.000000000000000444 ) ;
#9974=CARTESIAN_POINT ( 'NONE',  ( 94.20708369096698220, -27.10035099198479358, -13.29271931396930739 ) ) ;
#10000=DIRECTION ( 'NONE',  ( 0.000000000000000000, -0.9242245927363027524, -0.3818493186865928868 ) ) ;
#10021=ORIENTED_EDGE ( 'NONE', *, *, #37008, .F. ) ;
#10023=EDGE_CURVE ( 'NONE', #41036, #5448, #30538, .T. ) ;
#10028=DIRECTION ( 'NONE',  ( 1.000000000000000000, 0.000000000000000000, -0.000000000000000000 ) ) ;
#10052=CARTESIAN_POINT ( 'NONE',  ( 94.20708369096698220, -25.99489077589524300, -13.39321520033831447 ) ) ;
#10062=EDGE_LOOP ( 'NONE', ( #44352, #3324, #44313, #29892, #8402, #12885 ) ) ;
#10070=LINE ( 'NONE', #14140, #37326 ) ;
#10088=EDGE_CURVE ( 'NONE', #12518, #7405, #7790, .T. ) ;
#10101=LINE ( 'NONE', #38112, #6724 ) ;
#10111=ADVANCED_FACE ( 'NONE', ( #32173 ), #32621, .T. ) ;
#10116=FACE_OUTER_BOUND ( 'NONE', #44753, .T. ) ;
#10127=ORIENTED_EDGE ( 'NONE', *, *, #44846, .F. ) ;
#10139=VERTEX_POINT ( 'NONE', #39245 ) ;
#10151=CARTESIAN_POINT ( 'NONE',  ( 84.77016061404391678, -26.60966817898065884, -11.90521360603286816 ) ) ;
#10155=ORIENTED_EDGE ( 'NONE', *, *, #28971, .F. ) ;
#10162=CARTESIAN_POINT ( 'NONE',  ( 95.62170725701103891, -25.82400229693143245, -12.45813257048188660 ) ) ;
#10180=EDGE_CURVE ( 'NONE', #35146, #22099, #43119, .T. ) ;
#10192=CARTESIAN_POINT ( 'NONE',  ( 121.9470836909669913, -24.14644159042263993, -12.62951656296512937 ) ) ;
#10195=CARTESIAN_POINT ( 'NONE',  ( 86.75477599865929790, -26.60966817898065884, -11.90521360603286816 ) ) ;
#10198=DIRECTION ( 'NONE',  ( 0.000000000000000000, -0.9242245927363028635, -0.3818493186865930533 ) ) ;
#10202=LINE ( 'NONE', #21118, #9081 ) ;
#10211=DIRECTION ( 'NONE',  ( 0.000000000000000000, -0.9242245927363028635, -0.3818493186865927758 ) ) ;
#10216=CARTESIAN_POINT ( 'NONE',  ( 84.10862215250544693, -25.99489077589524300, -13.39321520033831625 ) ) ;
#10225=DIRECTION ( 'NONE',  ( 0.000000000000000000, 0.3818493186865928868, -0.9242245927363029745 ) ) ;
#10226=ORIENTED_EDGE ( 'NONE', *, *, #4690, .T. ) ;
#10228=VECTOR ( 'NONE', #33261, 1000.000000000000000 ) ;
#10247=DIRECTION ( 'NONE',  ( 1.000000000000000000, 0.000000000000000000, -0.000000000000000000 ) ) ;
#10254=DIRECTION ( 'NONE',  ( -0.4461977533474357216, 0.8271203734159379151, 0.3417300876246931463 ) ) ;
#10263=EDGE_CURVE ( 'NONE', #28337, #21924, #24894, .T. ) ;
#10277=ORIENTED_EDGE ( 'NONE', *, *, #42588, .F. ) ;
#10283=CARTESIAN_POINT ( 'NONE',  ( 84.77016061404391678, -25.99489077589524300, -13.39321520033831625 ) ) ;
#10285=DIRECTION ( 'NONE',  ( -0.8949343913984424415, 0.1703803081152067966, -0.4123869368673871993 ) ) ;
#10288=EDGE_CURVE ( 'NONE', #38132, #10759, #12060, .T. ) ;
#10295=EDGE_CURVE ( 'NONE', #14305, #30603, #2138, .T. ) ;
#10298=ADVANCED_FACE ( 'NONE', ( #18118 ), #28836, .T. ) ;
#10356=ADVANCED_FACE ( 'NONE', ( #21313 ), #10613, .T. ) ;
#10377=FACE_OUTER_BOUND ( 'NONE', #9362, .T. ) ;
#10382=CARTESIAN_POINT ( 'NONE',  ( 94.20708369096698220, -25.77760949922539879, -12.57042127303408385 ) ) ;
#10405=AXIS2_PLACEMENT_3D ( 'NONE', #14464, #24507, #18109 ) ;
#10418=LINE ( 'NONE', #9974, #18547 ) ;
#10430=DIRECTION ( 'NONE',  ( 0.000000000000000000, 0.9242245927363041957, 0.3818493186865896116 ) ) ;
#10449=AXIS2_PLACEMENT_3D ( 'NONE', #36622, #36395, #9052 ) ;
#10470=LINE ( 'NONE', #10909, #8545 ) ;
#10486=CARTESIAN_POINT ( 'NONE',  ( 88.07785292173620917, -25.99489077589524300, -13.39321520033831625 ) ) ;
#10496=AXIS2_PLACEMENT_3D ( 'NONE', #23079, #23769, #13049 ) ;
#10499=VERTEX_POINT ( 'NONE', #2069 ) ;
#10504=DIRECTION ( 'NONE',  ( 0.000000000000000000, -0.3818493186865927203, 0.9242245927363029745 ) ) ;
#10506=CARTESIAN_POINT ( 'NONE',  ( 95.62170725701116680, -25.21382792434065934, -13.93499303194756678 ) ) ;
#10527=DIRECTION ( 'NONE',  ( 0.8949343913984423304, 0.1703803081152067689, -0.4123869368673877545 ) ) ;
#10548=ADVANCED_FACE ( 'NONE', ( #10842 ), #37823, .T. ) ;
#10580=ORIENTED_EDGE ( 'NONE', *, *, #16967, .F. ) ;
#10583=EDGE_CURVE ( 'NONE', #37160, #42815, #18176, .T. ) ;
#10584=AXIS2_PLACEMENT_3D ( 'NONE', #2541, #13724, #34664 ) ;
#10595=DIRECTION ( 'NONE',  ( 0.000000000000000000, -0.3818493186865927203, 0.9242245927363029745 ) ) ;
#10599=LINE ( 'NONE', #21522, #26902 ) ;
#10605=FACE_OUTER_BOUND ( 'NONE', #21746, .T. ) ;
#10613=CYLINDRICAL_SURFACE ( 'NONE', #20376, 1.999999999999998890 ) ;
#10631=CARTESIAN_POINT ( 'NONE',  ( 90.99708770779186295, -27.84333996136784961, -14.15691383771150136 ) ) ;
#10658=AXIS2_PLACEMENT_3D ( 'NONE', #7290, #39203, #28507 ) ;
#10671=DIRECTION ( 'NONE',  ( 0.000000000000000000, -0.3818493186865936084, 0.9242245927363024194 ) ) ;
#10708=CYLINDRICAL_SURFACE ( 'NONE', #37828, 1.999999999999998890 ) ;
#10710=CARTESIAN_POINT ( 'NONE',  ( 91.65862616933031859, -25.99489077589524300, -13.39321520033831447 ) ) ;
#10712=ORIENTED_EDGE ( 'NONE', *, *, #15239, .T. ) ;
#10720=DIRECTION ( 'NONE',  ( -0.5735764363510446051, 0.3127926500124816878, -0.7570804645221042017 ) ) ;
#10727=DIRECTION ( 'NONE',  ( 1.000000000000000000, 0.000000000000000000, 0.000000000000000000 ) ) ;
#10759=VERTEX_POINT ( 'NONE', #3894 ) ;
#10765=DIRECTION ( 'NONE',  ( 0.000000000000000000, -0.3818493186865927203, 0.9242245927363029745 ) ) ;
#10767=VERTEX_POINT ( 'NONE', #14166 ) ;
#10778=DIRECTION ( 'NONE',  ( 0.000000000000000000, -0.9242245927363028635, -0.3818493186865930533 ) ) ;
#10814=CYLINDRICAL_SURFACE ( 'NONE', #25438, 1.999999999999998890 ) ;
#10833=DIRECTION ( 'NONE',  ( 1.000000000000000000, 0.000000000000000000, -0.000000000000000000 ) ) ;
#10842=FACE_OUTER_BOUND ( 'NONE', #3316, .T. ) ;
#10845=ORIENTED_EDGE ( 'NONE', *, *, #32665, .T. ) ;
#10851=ADVANCED_FACE ( 'NONE', ( #17814 ), #34908, .F. ) ;
#10869=DIRECTION ( 'NONE',  ( 0.000000000000000000, -0.3818493186865927203, 0.9242245927363029745 ) ) ;
#10889=LINE ( 'NONE', #43017, #22823 ) ;
#10890=ORIENTED_EDGE ( 'NONE', *, *, #29473, .T. ) ;
#10907=VERTEX_POINT ( 'NONE', #4113 ) ;
#10909=CARTESIAN_POINT ( 'NONE',  ( 121.9470836909669913, -29.69178914684045623, -14.92061247508468647 ) ) ;
#10920=DIRECTION ( 'NONE',  ( 0.000000000000000000, -0.3818493186865936084, 0.9242245927363024194 ) ) ;
#10927=LINE ( 'NONE', #35290, #19018 ) ;
#10936=LINE ( 'NONE', #437, #22441 ) ;
#10938=DIRECTION ( 'NONE',  ( 0.000000000000000000, -0.3818493186865936084, 0.9242245927363024194 ) ) ;
#10961=VERTEX_POINT ( 'NONE', #3459 ) ;
#10966=CIRCLE ( 'NONE', #26222, 2.000000000000000444 ) ;
#10970=DIRECTION ( 'NONE',  ( 0.000000000000000000, -0.3818493186865927203, 0.9242245927363029745 ) ) ;
#10979=CARTESIAN_POINT ( 'NONE',  ( 93.44708369096697709, -25.99489077589524300, -13.39321520033831447 ) ) ;
#10985=EDGE_CURVE ( 'NONE', #35430, #33401, #29194, .T. ) ;
#10992=DIRECTION ( 'NONE',  ( -0.5735764363510446051, 0.3127926500124816878, -0.7570804645221042017 ) ) ;
#11000=CARTESIAN_POINT ( 'NONE',  ( 91.65862616933031859, -24.14644159042263993, -12.62951656296512937 ) ) ;
#11013=ORIENTED_EDGE ( 'NONE', *, *, #35176, .F. ) ;
#11019=VECTOR ( 'NONE', #24170, 1000.000000000000000 ) ;
#11021=ADVANCED_FACE ( 'NONE', ( #32383 ), #15312, .T. ) ;
#11034=ORIENTED_EDGE ( 'NONE', *, *, #34241, .T. ) ;
#11048=VERTEX_POINT ( 'NONE', #15287 ) ;
#11056=DIRECTION ( 'NONE',  ( -0.000000000000000000, -0.3818493186865896671, 0.9242245927363040847 ) ) ;
#11060=EDGE_CURVE ( 'NONE', #42171, #26936, #2877, .T. ) ;
#11086=AXIS2_PLACEMENT_3D ( 'NONE', #21179, #38487, #34833 ) ;
#11103=FACE_OUTER_BOUND ( 'NONE', #15141, .T. ) ;
#11107=EDGE_CURVE ( 'NONE', #42191, #21542, #37128, .T. ) ;
#11114=EDGE_CURVE ( 'NONE', #3780, #4318, #14, .T. ) ;
#11143=DIRECTION ( 'NONE',  ( 0.000000000000000000, -0.9242245927363029745, -0.3818493186865927203 ) ) ;
#11153=DIRECTION ( 'NONE',  ( -1.000000000000000000, 0.000000000000000000, 0.000000000000000000 ) ) ;
#11154=AXIS2_PLACEMENT_3D ( 'NONE', #26153, #15671, #43491 ) ;
#11178=LINE ( 'NONE', #35544, #11368 ) ;
#11181=CIRCLE ( 'NONE', #43950, 2.000000000000000444 ) ;
#11188=DIRECTION ( 'NONE',  ( 0.000000000000000000, -0.9242245927363029745, -0.3818493186865927758 ) ) ;
#11190=AXIS2_PLACEMENT_3D ( 'NONE', #38038, #17511, #38467 ) ;
#11197=DIRECTION ( 'NONE',  ( -1.000000000000000000, 0.000000000000000000, 0.000000000000000000 ) ) ;
#11206=VERTEX_POINT ( 'NONE', #29652 ) ;
#11207=EDGE_CURVE ( 'NONE', #17, #2333, #7294, .T. ) ;
#11209=DIRECTION ( 'NONE',  ( 1.000000000000000000, 0.000000000000000000, -0.000000000000000000 ) ) ;
#11233=ORIENTED_EDGE ( 'NONE', *, *, #12476, .F. ) ;
#11260=VECTOR ( 'NONE', #8043, 1000.000000000000114 ) ;
#11274=EDGE_LOOP ( 'NONE', ( #24859, #4803, #32248, #19208, #15271 ) ) ;
#11304=DIRECTION ( 'NONE',  ( 0.000000000000000000, -0.3818493186865927203, 0.9242245927363029745 ) ) ;
#11321=DIRECTION ( 'NONE',  ( -0.8949343913984424415, -0.4123869368673878100, -0.1703803081152053811 ) ) ;
#11354=EDGE_LOOP ( 'NONE', ( #18321, #5491, #39145, #13144, #18243 ) ) ;
#11363=EDGE_CURVE ( 'NONE', #38132, #3542, #39331, .T. ) ;
#11366=AXIS2_PLACEMENT_3D ( 'NONE', #14047, #27964, #41871 ) ;
#11368=VECTOR ( 'NONE', #18467, 1000.000000000000114 ) ;
#11374=CARTESIAN_POINT ( 'NONE',  ( 88.35093386163799778, -27.84333996136784961, -14.15691383771150136 ) ) ;
#11384=DIRECTION ( 'NONE',  ( -1.000000000000000000, 0.000000000000000000, 0.000000000000000000 ) ) ;
#11418=ADVANCED_FACE ( 'NONE', ( #30109 ), #13241, .T. ) ;
#11421=EDGE_CURVE ( 'NONE', #37865, #7716, #9491, .T. ) ;
#11450=CARTESIAN_POINT ( 'NONE',  ( 90.33554924625337890, -25.99489077589524300, -13.39321520033831447 ) ) ;
#11452=ORIENTED_EDGE ( 'NONE', *, *, #36446, .T. ) ;
#11456=AXIS2_PLACEMENT_3D ( 'NONE', #16345, #20223, #26832 ) ;
#11478=DIRECTION ( 'NONE',  ( 0.5735764363510499342, 0.3127926500124801890, -0.7570804645221008711 ) ) ;
#11480=DIRECTION ( 'NONE',  ( -1.000000000000000000, 0.000000000000000000, 0.000000000000000000 ) ) ;
#11538=CARTESIAN_POINT ( 'NONE',  ( 93.24708369096698846, -25.99489077589524300, -13.39321520033831447 ) ) ;
#11544=EDGE_LOOP ( 'NONE', ( #16285, #11452, #2304, #14563, #16383 ) ) ;
#11576=LINE ( 'NONE', #35494, #30850 ) ;
#11577=ORIENTED_EDGE ( 'NONE', *, *, #30872, .F. ) ;
#11585=DIRECTION ( 'NONE',  ( 0.000000000000000000, -0.3818493186865927203, 0.9242245927363029745 ) ) ;
#11588=DIRECTION ( 'NONE',  ( 0.000000000000000000, -0.3818493186865927203, 0.9242245927363029745 ) ) ;
#11633=CARTESIAN_POINT ( 'NONE',  ( 90.04708369096697140, -25.99489077589524300, -13.39321520033831447 ) ) ;
#11643=AXIS2_PLACEMENT_3D ( 'NONE', #22958, #33202, #30028 ) ;
#11652=EDGE_CURVE ( 'NONE', #10767, #42505, #40808, .T. ) ;
#11740=ORIENTED_EDGE ( 'NONE', *, *, #19812, .T. ) ;
#11758=DIRECTION ( 'NONE',  ( 0.000000000000000000, -0.3818493186865929978, 0.9242245927363029745 ) ) ;
#11763=ORIENTED_EDGE ( 'NONE', *, *, #16387, .T. ) ;
#11769=EDGE_CURVE ( 'NONE', #40139, #30207, #4367, .T. ) ;
#11831=DIRECTION ( 'NONE',  ( 1.000000000000000000, 0.000000000000000000, -0.000000000000000000 ) ) ;
#11846=( NAMED_UNIT ( * ) SI_UNIT ( $, .STERADIAN. ) SOLID_ANGLE_UNIT ( ) );
#11860=ORIENTED_EDGE ( 'NONE', *, *, #25420, .T. ) ;
#11864=DIRECTION ( 'NONE',  ( 0.000000000000000000, 0.3818493186865929423, -0.9242245927363028635 ) ) ;
#11869=CARTESIAN_POINT ( 'NONE',  ( 94.20708369096698220, -26.70704619373760735, -14.24467064448769982 ) ) ;
#11870=CIRCLE ( 'NONE', #30815, 6.479565957685756494 ) ;
#11879=CARTESIAN_POINT ( 'NONE',  ( 95.28169473643895060, -24.52346489965341902, -16.95464091111045590 ) ) ;
#11911=PLANE ( 'NONE',  #7801 ) ;
#11916=ORIENTED_EDGE ( 'NONE', *, *, #16356, .T. ) ;
#11917=EDGE_LOOP ( 'NONE', ( #4535, #38810, #25970, #4118, #14545, #43036 ) ) ;
#11927=EDGE_CURVE ( 'NONE', #17, #36181, #30502, .T. ) ;
#11932=EDGE_CURVE ( 'NONE', #39770, #11206, #44453, .T. ) ;
#11933=EDGE_CURVE ( 'NONE', #39210, #12514, #14555, .T. ) ;
#11950=ORIENTED_EDGE ( 'NONE', *, *, #5000, .T. ) ;
#11976=VECTOR ( 'NONE', #36808, 1000.000000000000000 ) ;
#11983=ADVANCED_FACE ( 'NONE', ( #23678 ), #13881, .T. ) ;
#11987=DIRECTION ( 'NONE',  ( 0.000000000000000000, 0.9242245927363005320, 0.3818493186865984379 ) ) ;
#12015=ORIENTED_EDGE ( 'NONE', *, *, #5258, .T. ) ;
#12029=EDGE_CURVE ( 'NONE', #23066, #735, #4397, .T. ) ;
#12030=DIRECTION ( 'NONE',  ( 1.000000000000000000, 0.000000000000000000, -0.000000000000000000 ) ) ;
#12033=FACE_OUTER_BOUND ( 'NONE', #4346, .T. ) ;
#12040=CARTESIAN_POINT ( 'NONE',  ( 94.20708369096698220, -25.99489077589524300, -13.39321520033831447 ) ) ;
#12043=CARTESIAN_POINT ( 'NONE',  ( 90.33554924625337890, -25.23119213852205789, -15.24166438581092109 ) ) ;
#12048=EDGE_CURVE ( 'NONE', #35857, #23574, #5853, .T. ) ;
#12051=AXIS2_PLACEMENT_3D ( 'NONE', #42474, #1188, #15100 ) ;
#12057=CARTESIAN_POINT ( 'NONE',  ( 85.82015659721905365, -24.14644159042263993, -12.62951656296512937 ) ) ;
#12060=B_SPLINE_CURVE_WITH_KNOTS ( 'NONE', 3,
 ( #27496, #14249, #31342, #14029 ),
 .UNSPECIFIED., .F., .F.,
 ( 4, 4 ),
 ( 0.000000000000000000, 1.000000000000000000 ),
 .UNSPECIFIED. ) ;
#12073=DIRECTION ( 'NONE',  ( 1.000000000000000000, 0.000000000000000000, -0.000000000000000000 ) ) ;
#12102=DIRECTION ( 'NONE',  ( 0.000000000000000000, -0.3818493186865927203, 0.9242245927363029745 ) ) ;
#12147=ORIENTED_EDGE ( 'NONE', *, *, #25053, .F. ) ;
#12190=ORIENTED_EDGE ( 'NONE', *, *, #17038, .F. ) ;
#12208=CARTESIAN_POINT ( 'NONE',  ( 85.70478001548416103, -26.75858941326842810, -11.54476601486570964 ) ) ;
#12213=ADVANCED_FACE ( 'NONE', ( #19794 ), #20441, .T. ) ;
#12223=ADVANCED_FACE ( 'NONE', ( #27766 ), #8763, .T. ) ;
#12230=DIRECTION ( 'NONE',  ( 0.000000000000000000, 0.3818493186865927203, -0.9242245927363029745 ) ) ;
#12232=AXIS2_PLACEMENT_3D ( 'NONE', #37935, #13330, #3053 ) ;
#12241=VERTEX_POINT ( 'NONE', #20921 ) ;
#12244=EDGE_CURVE ( 'NONE', #24220, #36515, #31350, .T. ) ;
#12270=CARTESIAN_POINT ( 'NONE',  ( 86.75477599865929790, -25.99489077589524300, -13.39321520033831625 ) ) ;
#12285=CARTESIAN_POINT ( 'NONE',  ( 88.07785292173620917, -25.38011337280982715, -14.88121679464376257 ) ) ;
#12288=ORIENTED_EDGE ( 'NONE', *, *, #1363, .T. ) ;
#12295=VERTEX_POINT ( 'NONE', #23331 ) ;
#12301=DIRECTION ( 'NONE',  ( -0.000000000000000000, -0.3818493186865928313, 0.9242245927363027524 ) ) ;
#12317=DIRECTION ( 'NONE',  ( 0.000000000000000000, -0.9242245927363028635, -0.3818493186865930533 ) ) ;
#12341=B_SPLINE_CURVE_WITH_KNOTS ( 'NONE', 3,
 ( #10382, #34524, #10162, #3301 ),
 .UNSPECIFIED., .F., .F.,
 ( 4, 4 ),
 ( 0.000000000000000000, 1.000000000000000000 ),
 .UNSPECIFIED. ) ;
#12353=DIRECTION ( 'NONE',  ( 0.000000000000000000, 0.9242245927363034186, 0.3818493186865916655 ) ) ;
#12359=VECTOR ( 'NONE', #38787, 1000.000000000000000 ) ;
#12375=AXIS2_PLACEMENT_3D ( 'NONE', #42185, #21649, #10727 ) ;
#12390=CARTESIAN_POINT ( 'NONE',  ( 89.40092984481313465, -25.99489077589524300, -13.39321520033831625 ) ) ;
#12413=ORIENTED_EDGE ( 'NONE', *, *, #15719, .T. ) ;
#12417=ADVANCED_FACE ( 'NONE', ( #10116 ), #38130, .F. ) ;
#12422=AXIS2_PLACEMENT_3D ( 'NONE', #45095, #13852, #17718 ) ;
#12426=CARTESIAN_POINT ( 'NONE',  ( 94.20708369096698220, -26.42437990495228917, -14.12788525418686270 ) ) ;
#12440=DIRECTION ( 'NONE',  ( 1.000000000000000000, 0.000000000000000000, -0.000000000000000000 ) ) ;
#12463=CARTESIAN_POINT ( 'NONE',  ( 121.9470836909669913, -24.14644159042263993, -12.62951656296512937 ) ) ;
#12466=CYLINDRICAL_SURFACE ( 'NONE', #5370, 1.999999999999998890 ) ;
#12467=ORIENTED_EDGE ( 'NONE', *, *, #16395, .T. ) ;
#12476=EDGE_CURVE ( 'NONE', #18672, #39054, #22599, .T. ) ;
#12480=LINE ( 'NONE', #2193, #26453 ) ;
#12499=EDGE_CURVE ( 'NONE', #19531, #39489, #40072, .T. ) ;
#12512=DIRECTION ( 'NONE',  ( 0.000000000000000000, -0.3818493186865927203, 0.9242245927363029745 ) ) ;
#12514=VERTEX_POINT ( 'NONE', #5655 ) ;
#12518=VERTEX_POINT ( 'NONE', #37578 ) ;
#12532=LINE ( 'NONE', #5220, #31573 ) ;
#12536=DIRECTION ( 'NONE',  ( 0.000000000000000000, -0.9242245927363029745, -0.3818493186865927758 ) ) ;
#12557=CARTESIAN_POINT ( 'NONE',  ( 94.99177781699742695, -25.99489077589524300, -13.39321520033831447 ) ) ;
#12562=DIRECTION ( 'NONE',  ( 0.000000000000000000, 0.3818493186865928868, -0.9242245927363027524 ) ) ;
#12566=DIRECTION ( 'NONE',  ( 1.000000000000000000, 0.000000000000000000, -0.000000000000000000 ) ) ;
#12587=VECTOR ( 'NONE', #28371, 1000.000000000000114 ) ;
#12597=CIRCLE ( 'NONE', #38063, 2.000000000000000444 ) ;
#12617=VECTOR ( 'NONE', #4865, 1000.000000000000114 ) ;
#12674=ORIENTED_EDGE ( 'NONE', *, *, #24470, .T. ) ;
#12682=CARTESIAN_POINT ( 'NONE',  ( 83.83554121260367253, -25.99489077589524300, -13.39321520033831625 ) ) ;
#12683=DIRECTION ( 'NONE',  ( 0.000000000000000000, -0.3818493186865927203, 0.9242245927363029745 ) ) ;
#12713=DIRECTION ( 'NONE',  ( 1.000000000000000000, 0.000000000000000000, -0.000000000000000000 ) ) ;
#12755=CARTESIAN_POINT ( 'NONE',  ( 121.9470836909669913, -25.99489077589524300, -13.39321520033831447 ) ) ;
#12770=CIRCLE ( 'NONE', #31692, 2.000000000000000444 ) ;
#12772=CARTESIAN_POINT ( 'NONE',  ( 91.11246428952674137, -25.99489077589524300, -13.39321520033831625 ) ) ;
#12816=ADVANCED_FACE ( 'NONE', ( #25395 ), #31546, .T. ) ;
#12828=FACE_OUTER_BOUND ( 'NONE', #15522, .T. ) ;
#12838=ORIENTED_EDGE ( 'NONE', *, *, #39328, .F. ) ;
#12842=DIRECTION ( 'NONE',  ( 0.000000000000000000, 0.3818493186865929423, -0.9242245927363027524 ) ) ;
#12856=CARTESIAN_POINT ( 'NONE',  ( 96.23375075340858587, -26.75621354156143994, -11.55051655297938318 ) ) ;
#12859=CARTESIAN_POINT ( 'NONE',  ( 87.14323352029596492, -25.99489077589524300, -13.39321520033831625 ) ) ;
#12862=AXIS2_PLACEMENT_3D ( 'NONE', #41799, #16730, #27440 ) ;
#12871=VERTEX_POINT ( 'NONE', #44472 ) ;
#12885=ORIENTED_EDGE ( 'NONE', *, *, #13638, .F. ) ;
#12888=AXIS2_PLACEMENT_3D ( 'NONE', #5338, #42973, #29732 ) ;
#12912=DIRECTION ( 'NONE',  ( 0.5735764363510498232, -0.3127926500124802445, 0.7570804645221007600 ) ) ;
#12933=ADVANCED_FACE ( 'NONE', ( #5923 ), #2205, .T. ) ;
#12943=CARTESIAN_POINT ( 'NONE',  ( 121.9470836909669913, -27.84333996136784961, -14.15691383771150136 ) ) ;
#12953=ORIENTED_EDGE ( 'NONE', *, *, #27344, .T. ) ;
#12976=VERTEX_POINT ( 'NONE', #37387 ) ;
#13000=CARTESIAN_POINT ( 'NONE',  ( 121.9470836909669913, -27.84333996136784961, -14.15691383771150136 ) ) ;
#13012=DIRECTION ( 'NONE',  ( 0.5735764363510499342, 0.3127926500124801890, -0.7570804645221008711 ) ) ;
#13015=EDGE_LOOP ( 'NONE', ( #25591, #24673, #30668, #9094, #21520, #36920 ) ) ;
#13019=EDGE_CURVE ( 'NONE', #15443, #17364, #44928, .T. ) ;
#13030=CARTESIAN_POINT ( 'NONE',  ( 89.01247232317646763, -24.14644159042263993, -12.62951656296512937 ) ) ;
#13042=EDGE_CURVE ( 'NONE', #24400, #38783, #16822, .T. ) ;
#13044=ORIENTED_EDGE ( 'NONE', *, *, #14764, .F. ) ;
#13049=DIRECTION ( 'NONE',  ( 0.000000000000000000, -0.3818493186865927203, 0.9242245927363029745 ) ) ;
#13058=ORIENTED_EDGE ( 'NONE', *, *, #8377, .F. ) ;
#13069=EDGE_CURVE ( 'NONE', #29689, #7697, #10927, .T. ) ;
#13085=CIRCLE ( 'NONE', #38528, 0.8509999999999994236 ) ;
#13105=CARTESIAN_POINT ( 'NONE',  ( 94.20708369096698220, -25.99489077589524300, -13.39321520033831447 ) ) ;
#13127=ADVANCED_FACE ( 'NONE', ( #427 ), #30680, .T. ) ;
#13144=ORIENTED_EDGE ( 'NONE', *, *, #12499, .F. ) ;
#13157=FACE_OUTER_BOUND ( 'NONE', #31083, .T. ) ;
#13168=ADVANCED_FACE ( 'NONE', ( #42389 ), #28465, .T. ) ;
#13169=DIRECTION ( 'NONE',  ( -1.000000000000000000, 0.000000000000000000, 0.000000000000000000 ) ) ;
#13193=AXIS2_PLACEMENT_3D ( 'NONE', #10216, #12566, #24124 ) ;
#13196=DIRECTION ( 'NONE',  ( 1.000000000000000000, 0.000000000000000000, -0.000000000000000000 ) ) ;
#13199=VERTEX_POINT ( 'NONE', #34838 ) ;
#13213=DIRECTION ( 'NONE',  ( -0.5735764363510450492, -0.3127926500124816878, 0.7570804645221038687 ) ) ;
#13218=ORIENTED_EDGE ( 'NONE', *, *, #7588, .F. ) ;
#13220=CARTESIAN_POINT ( 'NONE',  ( 87.80477198183443477, -25.99489077589524300, -13.39321520033831625 ) ) ;
#13234=ORIENTED_EDGE ( 'NONE', *, *, #34763, .T. ) ;
#13241=PLANE ( 'NONE',  #34212 ) ;
#13243=ORIENTED_EDGE ( 'NONE', *, *, #16294, .T. ) ;
#13273=DIRECTION ( 'NONE',  ( 1.000000000000000000, 0.000000000000000000, -0.000000000000000000 ) ) ;
#13275=DIRECTION ( 'NONE',  ( 1.000000000000000000, 0.000000000000000000, -0.000000000000000000 ) ) ;
#13278=CIRCLE ( 'NONE', #11086, 3.853420195439741125 ) ;
#13288=DIRECTION ( 'NONE',  ( 0.000000000000000000, 0.9242245927363029745, 0.3818493186865928868 ) ) ;
#13306=CARTESIAN_POINT ( 'NONE',  ( 94.20708369096698220, -25.99489077589524300, -13.39321520033831447 ) ) ;
#13308=CIRCLE ( 'NONE', #30019, 2.000000000000000444 ) ;
#13330=DIRECTION ( 'NONE',  ( 1.000000000000000000, 0.000000000000000000, -0.000000000000000000 ) ) ;
#13335=DIRECTION ( 'NONE',  ( -0.5735764363510450492, -0.3127926500124816878, 0.7570804645221038687 ) ) ;
#13344=DIRECTION ( 'NONE',  ( -0.8949343913984424415, 0.4123869368673878100, 0.1703803081152053811 ) ) ;
#13347=DIRECTION ( 'NONE',  ( -1.000000000000000000, 0.000000000000000000, 0.000000000000000000 ) ) ;
#13360=EDGE_CURVE ( 'NONE', #44289, #30333, #40110, .T. ) ;
#13389=ORIENTED_EDGE ( 'NONE', *, *, #45120, .F. ) ;
#13390=ADVANCED_FACE ( 'NONE', ( #8178 ), #37190, .T. ) ;
#13399=CARTESIAN_POINT ( 'NONE',  ( 94.20708369096698220, -26.72956082974378944, -12.96372607128127363 ) ) ;
#13411=DIRECTION ( 'NONE',  ( 1.000000000000000000, 0.000000000000000000, -0.000000000000000000 ) ) ;
#13419=VERTEX_POINT ( 'NONE', #32560 ) ;
#13435=EDGE_CURVE ( 'NONE', #28262, #15443, #5172, .T. ) ;
#13439=ORIENTED_EDGE ( 'NONE', *, *, #41794, .T. ) ;
#13445=LINE ( 'NONE', #23247, #27456 ) ;
#13448=ADVANCED_FACE ( 'NONE', ( #22310 ), #3712, .T. ) ;
#13452=STYLED_ITEM('',(#45190),#36189);
#13477=ORIENTED_EDGE ( 'NONE', *, *, #22503, .T. ) ;
#13533=CARTESIAN_POINT ( 'NONE',  ( 83.83554121260367253, -24.14644159042263993, -12.62951656296512937 ) ) ;
#13545=VERTEX_POINT ( 'NONE', #12057 ) ;
#13562=ORIENTED_EDGE ( 'NONE', *, *, #14431, .T. ) ;
#13563=CARTESIAN_POINT ( 'NONE',  ( 86.09323753712084226, -25.38011337280982715, -14.88121679464376257 ) ) ;
#13586=CARTESIAN_POINT ( 'NONE',  ( 90.04708369096697140, -25.79823837677164988, -13.86919086559751157 ) ) ;
#13605=VERTEX_POINT ( 'NONE', #12285 ) ;
#13608=EDGE_CURVE ( 'NONE', #4544, #18037, #36484, .T. ) ;
#13609=VECTOR ( 'NONE', #30403, 1000.000000000000114 ) ;
#13610=DIRECTION ( 'NONE',  ( 0.000000000000000000, -0.3818493186865936084, 0.9242245927363024194 ) ) ;
#13613=ADVANCED_FACE ( 'NONE', ( #5642 ), #32997, .T. ) ;
#13638=EDGE_CURVE ( 'NONE', #20846, #39210, #33540, .T. ) ;
#13645=EDGE_CURVE ( 'NONE', #38363, #8089, #785, .T. ) ;
#13662=DIRECTION ( 'NONE',  ( 1.000000000000000000, 0.000000000000000000, -0.000000000000000000 ) ) ;
#13686=CARTESIAN_POINT ( 'NONE',  ( 87.41631446019775353, -25.38011337280982715, -14.88121679464376257 ) ) ;
#13724=DIRECTION ( 'NONE',  ( 1.000000000000000000, 0.000000000000000000, -0.000000000000000000 ) ) ;
#13776=ORIENTED_EDGE ( 'NONE', *, *, #6315, .F. ) ;
#13788=DIRECTION ( 'NONE',  ( 1.000000000000000000, 0.000000000000000000, -0.000000000000000000 ) ) ;
#13792=ORIENTED_EDGE ( 'NONE', *, *, #42112, .T. ) ;
#13803=LINE ( 'NONE', #23165, #42738 ) ;
#13805=ADVANCED_FACE ( 'NONE', ( #39306 ), #42325, .T. ) ;
#13837=CARTESIAN_POINT ( 'NONE',  ( 90.06246830635160450, -25.99489077589524300, -13.39321520033831625 ) ) ;
#13852=DIRECTION ( 'NONE',  ( -1.000000000000000000, 0.000000000000000000, 0.000000000000000000 ) ) ;
#13854=PLANE ( 'NONE',  #24752 ) ;
#13873=DIRECTION ( 'NONE',  ( 1.000000000000000000, 0.000000000000000000, -0.000000000000000000 ) ) ;
#13881=CONICAL_SURFACE ( 'NONE', #34246, 1.610000000000000986, 0.9599310885968765916 ) ;
#13892=CARTESIAN_POINT ( 'NONE',  ( 96.54708369096698561, -23.81115550238859413, -13.04821483042134389 ) ) ;
#13898=VERTEX_POINT ( 'NONE', #20087 ) ;
#13904=ORIENTED_EDGE ( 'NONE', *, *, #23358, .T. ) ;
#13921=CARTESIAN_POINT ( 'NONE',  ( 96.46827370896536991, -25.18754255092518335, -13.99861390895580371 ) ) ;
#13926=CIRCLE ( 'NONE', #32096, 1.610000000000000986 ) ;
#13930=VECTOR ( 'NONE', #25326, 1000.000000000000000 ) ;
#13936=ORIENTED_EDGE ( 'NONE', *, *, #5000, .F. ) ;
#13942=CARTESIAN_POINT ( 'NONE',  ( 87.68939540009954214, -25.99489077589524300, -13.39321520033831447 ) ) ;
#13949=EDGE_CURVE ( 'NONE', #22858, #44020, #21228, .T. ) ;
#13982=CARTESIAN_POINT ( 'NONE',  ( 83.83554121260367253, -25.23119213852205789, -15.24166438581092109 ) ) ;
#13985=PLANE ( 'NONE',  #9964 ) ;
#13988=CIRCLE ( 'NONE', #19814, 1.610000000000000986 ) ;
#13994=ORIENTED_EDGE ( 'NONE', *, *, #3118, .F. ) ;
#13995=DIRECTION ( 'NONE',  ( 0.000000000000000000, 0.3818493186865927203, -0.9242245927363029745 ) ) ;
#13998=EDGE_CURVE ( 'NONE', #17646, #21796, #31408, .T. ) ;
#14000=CARTESIAN_POINT ( 'NONE',  ( 86.48169505875749508, -24.14644159042263993, -12.62951656296512937 ) ) ;
#14009=VECTOR ( 'NONE', #11321, 1000.000000000000114 ) ;
#14015=DIRECTION ( 'NONE',  ( 1.000000000000000000, 0.000000000000000000, -0.000000000000000000 ) ) ;
#14029=CARTESIAN_POINT ( 'NONE',  ( 96.46827370896536991, -26.99359428275991846, -13.24861209478998170 ) ) ;
#14047=CARTESIAN_POINT ( 'NONE',  ( 90.48265143217095385, -25.18747534170762492, -13.05962633474799439 ) ) ;
#14048=CARTESIAN_POINT ( 'NONE',  ( 87.02785693856107230, -25.23119213852205789, -15.24166438581092109 ) ) ;
#14049=VECTOR ( 'NONE', #11478, 1000.000000000000000 ) ;
#14055=CARTESIAN_POINT ( 'NONE',  ( 96.46827370896536991, -26.80223900086530264, -12.78781649172082879 ) ) ;
#14059=CARTESIAN_POINT ( 'NONE',  ( 96.54708369096698561, -27.29184247633061489, -11.60278472507885894 ) ) ;
#14062=ORIENTED_EDGE ( 'NONE', *, *, #30487, .T. ) ;
#14065=DIRECTION ( 'NONE',  ( 0.000000000000000000, 0.3818493186865927203, -0.9242245927363029745 ) ) ;
#14077=CARTESIAN_POINT ( 'NONE',  ( 87.41631446019775353, -26.60966817898065884, -11.90521360603286816 ) ) ;
#14082=ORIENTED_EDGE ( 'NONE', *, *, #39569, .T. ) ;
#14097=DIRECTION ( 'NONE',  ( 1.000000000000000000, 0.000000000000000000, -0.000000000000000000 ) ) ;
#14103=DIRECTION ( 'NONE',  ( 1.000000000000000000, 0.000000000000000000, -0.000000000000000000 ) ) ;
#14119=DIRECTION ( 'NONE',  ( 0.000000000000000000, 0.3818493186865927203, -0.9242245927363029745 ) ) ;
#14120=DIRECTION ( 'NONE',  ( 1.000000000000000000, 0.000000000000000000, -0.000000000000000000 ) ) ;
#14128=LINE ( 'NONE', #24618, #16628 ) ;
#14129=AXIS2_PLACEMENT_3D ( 'NONE', #22848, #13275, #23545 ) ;
#14140=CARTESIAN_POINT ( 'NONE',  ( 90.72400676789006013, -25.38011337280982715, -14.88121679464376257 ) ) ;
#14145=LINE ( 'NONE', #41969, #43100 ) ;
#14166=CARTESIAN_POINT ( 'NONE',  ( 91.65862616933031859, -25.23119213852205789, -15.24166438581092109 ) ) ;
#14196=ADVANCED_FACE ( 'NONE', ( #30203, #26100 ), #9232, .F. ) ;
#14227=AXIS2_PLACEMENT_3D ( 'NONE', #34273, #17626, #44786 ) ;
#14229=DIRECTION ( 'NONE',  ( 0.000000000000000000, -0.3818493186865927203, 0.9242245927363029745 ) ) ;
#14249=CARTESIAN_POINT ( 'NONE',  ( 94.86797725101186529, -26.87133687923154923, -13.19810066433400664 ) ) ;
#14261=EDGE_CURVE ( 'NONE', #4162, #8497, #4459, .T. ) ;
#14264=VECTOR ( 'NONE', #672, 1000.000000000000114 ) ;
#14271=AXIS2_PLACEMENT_3D ( 'NONE', #22927, #30450, #19291 ) ;
#14272=DIRECTION ( 'NONE',  ( 1.000000000000000000, 0.000000000000000000, -0.000000000000000000 ) ) ;
#14278=AXIS2_PLACEMENT_3D ( 'NONE', #24874, #22127, #7536 ) ;
#14279=LINE ( 'NONE', #17476, #27411 ) ;
#14282=DIRECTION ( 'NONE',  ( 0.000000000000000000, -0.3818493186865927203, 0.9242245927363029745 ) ) ;
#14289=AXIS2_PLACEMENT_3D ( 'NONE', #33089, #19210, #2715 ) ;
#14299=PRODUCT ( 'Reach Screw', 'Reach Screw', '', ( #44614 ) ) ;
#14305=VERTEX_POINT ( 'NONE', #29974 ) ;
#14315=VECTOR ( 'NONE', #35685, 1000.000000000000000 ) ;
#14319=ORIENTED_EDGE ( 'NONE', *, *, #44180, .F. ) ;
#14343=VECTOR ( 'NONE', #44371, 1000.000000000000114 ) ;
#14373=EDGE_LOOP ( 'NONE', ( #33181, #24198, #27696, #39281, #26711 ) ) ;
#14400=CIRCLE ( 'NONE', #27506, 2.000000000000000444 ) ;
#14419=DIRECTION ( 'NONE',  ( 1.000000000000000000, 0.000000000000000000, -0.000000000000000000 ) ) ;
#14431=EDGE_CURVE ( 'NONE', #14958, #32925, #6659, .T. ) ;
#14434=VERTEX_POINT ( 'NONE', #14000 ) ;
#14450=EDGE_CURVE ( 'NONE', #3542, #33593, #17588, .T. ) ;
#14459=LINE ( 'NONE', #25175, #30543 ) ;
#14464=CARTESIAN_POINT ( 'NONE',  ( 84.10862215250544693, -25.99489077589524300, -13.39321520033831625 ) ) ;
#14473=DIRECTION ( 'NONE',  ( 1.000000000000000000, 0.000000000000000000, -0.000000000000000000 ) ) ;
#14496=CARTESIAN_POINT ( 'NONE',  ( 87.68939540009954214, -25.99489077589524300, -13.39321520033831447 ) ) ;
#14539=DIRECTION ( 'NONE',  ( 1.000000000000000000, 0.000000000000000000, -0.000000000000000000 ) ) ;
#14545=ORIENTED_EDGE ( 'NONE', *, *, #12048, .F. ) ;
#14555=CIRCLE ( 'NONE', #40847, 2.000000000000000444 ) ;
#14563=ORIENTED_EDGE ( 'NONE', *, *, #28153, .F. ) ;
#14566=DIRECTION ( 'NONE',  ( 0.000000000000000000, -0.3818493186865936084, 0.9242245927363024194 ) ) ;
#14568=CIRCLE ( 'NONE', #31321, 2.000000000000000444 ) ;
#14571=ORIENTED_EDGE ( 'NONE', *, *, #40533, .T. ) ;
#14584=DIRECTION ( 'NONE',  ( 0.000000000000000000, -0.3818493186865927203, 0.9242245927363029745 ) ) ;
#14596=VERTEX_POINT ( 'NONE', #3060 ) ;
#14618=ORIENTED_EDGE ( 'NONE', *, *, #10088, .F. ) ;
#14619=VERTEX_POINT ( 'NONE', #44573 ) ;
#14639=CIRCLE ( 'NONE', #6640, 2.000000000000000444 ) ;
#14645=UNCERTAINTY_MEASURE_WITH_UNIT (LENGTH_MEASURE( 1.000000000000000082E-05 ), #31677, 'distance_accuracy_value', 'NONE');
#14648=ORIENTED_EDGE ( 'NONE', *, *, #4136, .F. ) ;
#14657=VERTEX_POINT ( 'NONE', #18621 ) ;
#14658=EDGE_LOOP ( 'NONE', ( #29678, #5936, #43033, #1019, #3286, #25358 ) ) ;
#14665=CARTESIAN_POINT ( 'NONE',  ( 91.77400275106518279, -26.75858941326842810, -11.54476601486570964 ) ) ;
#14678=CARTESIAN_POINT ( 'NONE',  ( 88.35093386163799778, -25.99489077589524300, -13.39321520033831447 ) ) ;
#14680=ORIENTED_EDGE ( 'NONE', *, *, #29792, .F. ) ;
#14691=CARTESIAN_POINT ( 'NONE',  ( 85.15861813568058380, -25.99489077589524300, -13.39321520033831625 ) ) ;
#14747=DIRECTION ( 'NONE',  ( 1.000000000000000000, 0.000000000000000000, -0.000000000000000000 ) ) ;
#14764=EDGE_CURVE ( 'NONE', #27606, #25132, #25599, .T. ) ;
#14773=ORIENTED_EDGE ( 'NONE', *, *, #902, .F. ) ;
#14798=DIRECTION ( 'NONE',  ( 0.000000000000000000, -0.3818493186865927203, 0.9242245927363029745 ) ) ;
#14814=PRESENTATION_STYLE_ASSIGNMENT (( #39433 ) ) ;
#14822=CIRCLE ( 'NONE', #3871, 2.000000000000000444 ) ;
#14826=ORIENTED_EDGE ( 'NONE', *, *, #3062, .F. ) ;
#14832=CONICAL_SURFACE ( 'NONE', #22089, 2.000000000000000444, 0.9599310885968830309 ) ;
#14846=CARTESIAN_POINT ( 'NONE',  ( 90.99708770779186295, -25.99489077589524300, -13.39321520033831447 ) ) ;
#14848=ORIENTED_EDGE ( 'NONE', *, *, #11927, .T. ) ;
#14875=ORIENTED_EDGE ( 'NONE', *, *, #29390, .T. ) ;
#14878=CARTESIAN_POINT ( 'NONE',  ( 121.9470836909669913, -24.14644159042263993, -12.62951656296512937 ) ) ;
#14890=CARTESIAN_POINT ( 'NONE',  ( 86.48169505875749508, -26.75858941326842810, -11.54476601486570964 ) ) ;
#14903=CIRCLE ( 'NONE', #4710, 2.000000000000000444 ) ;
#14910=DIRECTION ( 'NONE',  ( 1.000000000000000000, 0.000000000000000000, -0.000000000000000000 ) ) ;
#14915=AXIS2_PLACEMENT_3D ( 'NONE', #38431, #13169, #16590 ) ;
#14916=DIRECTION ( 'NONE',  ( 1.000000000000000000, 0.000000000000000000, -0.000000000000000000 ) ) ;
#14930=EDGE_LOOP ( 'NONE', ( #27169, #23457, #44051, #39026, #40927 ) ) ;
#14941=AXIS2_PLACEMENT_3D ( 'NONE', #27586, #42159, #10920 ) ;
#14958=VERTEX_POINT ( 'NONE', #36726 ) ;
#15006=EDGE_CURVE ( 'NONE', #31353, #39217, #14145, .T. ) ;
#15021=DIRECTION ( 'NONE',  ( 0.000000000000000000, -0.3818493186865927203, 0.9242245927363029745 ) ) ;
#15045=CARTESIAN_POINT ( 'NONE',  ( 121.9470836909669913, -27.84333996136784961, -14.15691383771150136 ) ) ;
#15048=ORIENTED_EDGE ( 'NONE', *, *, #8299, .T. ) ;
#15055=ORIENTED_EDGE ( 'NONE', *, *, #1346, .T. ) ;
#15057=AXIS2_PLACEMENT_3D ( 'NONE', #43880, #2588, #34051 ) ;
#15060=AXIS2_PLACEMENT_3D ( 'NONE', #43465, #43238, #40264 ) ;
#15069=EDGE_CURVE ( 'NONE', #42332, #14596, #19806, .T. ) ;
#15100=DIRECTION ( 'NONE',  ( 0.000000000000000000, -0.3818493186865927203, 0.9242245927363029745 ) ) ;
#15103=CARTESIAN_POINT ( 'NONE',  ( 94.20708369096698220, -25.14343533174585943, -14.10537061818067883 ) ) ;
#15108=EDGE_LOOP ( 'NONE', ( #10127, #13234, #20910, #11013, #14680 ) ) ;
#15114=ADVANCED_FACE ( 'NONE', ( #38516 ), #43831, .F. ) ;
#15141=EDGE_LOOP ( 'NONE', ( #3043, #37982, #44866, #21265 ) ) ;
#15149=DIRECTION ( 'NONE',  ( 1.000000000000000000, 0.000000000000000000, -0.000000000000000000 ) ) ;
#15152=ORIENTED_EDGE ( 'NONE', *, *, #15652, .F. ) ;
#15173=DIRECTION ( 'NONE',  ( 1.000000000000000000, 0.000000000000000000, -0.000000000000000000 ) ) ;
#15174=CARTESIAN_POINT ( 'NONE',  ( 94.20708369096698220, -24.88943055980569241, -13.49371108670732333 ) ) ;
#15203=CARTESIAN_POINT ( 'NONE',  ( 90.45092582798827152, -25.99489077589524300, -13.39321520033831625 ) ) ;
#15226=DIRECTION ( 'NONE',  ( 1.000000000000000000, 0.000000000000000000, -0.000000000000000000 ) ) ;
#15233=CARTESIAN_POINT ( 'NONE',  ( 92.32016463086877422, -25.99489077589524300, -13.39321520033831447 ) ) ;
#15235=ORIENTED_EDGE ( 'NONE', *, *, #34761, .T. ) ;
#15239=EDGE_CURVE ( 'NONE', #12976, #41351, #30803, .T. ) ;
#15259=DIRECTION ( 'NONE',  ( 0.000000000000000000, -0.3818493186865927203, 0.9242245927363029745 ) ) ;
#15263=ORIENTED_EDGE ( 'NONE', *, *, #6178, .T. ) ;
#15271=ORIENTED_EDGE ( 'NONE', *, *, #6417, .F. ) ;
#15273=AXIS2_PLACEMENT_3D ( 'NONE', #31264, #25108, #17158 ) ;
#15275=FACE_OUTER_BOUND ( 'NONE', #42861, .T. ) ;
#15287=CARTESIAN_POINT ( 'NONE',  ( 92.32016463086877422, -25.23119213852205789, -15.24166438581092109 ) ) ;
#15292=EDGE_CURVE ( 'NONE', #31941, #21796, #4770, .T. ) ;
#15312=CONICAL_SURFACE ( 'NONE', #720, 2.000000000000000444, 0.9599310885968830309 ) ;
#15322=ORIENTED_EDGE ( 'NONE', *, *, #7754, .T. ) ;
#15323=AXIS2_PLACEMENT_3D ( 'NONE', #28187, #30932, #41872 ) ;
#15351=VECTOR ( 'NONE', #26364, 1000.000000000000000 ) ;
#15359=DIRECTION ( 'NONE',  ( -0.4461977533474357216, -0.8271203734159379151, -0.3417300876246930907 ) ) ;
#15380=AXIS2_PLACEMENT_3D ( 'NONE', #40089, #8850, #8406 ) ;
#15394=DIRECTION ( 'NONE',  ( 1.000000000000000000, 0.000000000000000000, 0.000000000000000000 ) ) ;
#15403=AXIS2_PLACEMENT_3D ( 'NONE', #5042, #32183, #4594 ) ;
#15438=AXIS2_PLACEMENT_3D ( 'NONE', #27391, #6639, #20770 ) ;
#15439=EDGE_CURVE ( 'NONE', #34542, #19992, #21982, .T. ) ;
#15442=DIRECTION ( 'NONE',  ( 1.000000000000000000, 0.000000000000000000, -0.000000000000000000 ) ) ;
#15443=VERTEX_POINT ( 'NONE', #35153 ) ;
#15446=ORIENTED_EDGE ( 'NONE', *, *, #35105, .F. ) ;
#15482=CIRCLE ( 'NONE', #36584, 0.8509999999999994236 ) ;
#15488=CARTESIAN_POINT ( 'NONE',  ( 83.72016463086879412, -25.99489077589524300, -13.39321520033831447 ) ) ;
#15503=DIRECTION ( 'NONE',  ( 1.000000000000000000, 0.000000000000000000, -0.000000000000000000 ) ) ;
#15522=EDGE_LOOP ( 'NONE', ( #11950, #5287, #32824, #36722 ) ) ;
#15541=ORIENTED_EDGE ( 'NONE', *, *, #35321, .T. ) ;
#15543=AXIS2_PLACEMENT_3D ( 'NONE', #33467, #13873, #28234 ) ;
#15561=EDGE_CURVE ( 'NONE', #22394, #7248, #13308, .T. ) ;
#15563=VECTOR ( 'NONE', #8925, 1000.000000000000000 ) ;
#15579=EDGE_CURVE ( 'NONE', #21542, #3446, #44619, .T. ) ;
#15596=DIRECTION ( 'NONE',  ( 0.000000000000000000, -0.9242245927363028635, -0.3818493186865930533 ) ) ;
#15600=ORIENTED_EDGE ( 'NONE', *, *, #11107, .T. ) ;
#15621=ADVANCED_BREP_SHAPE_REPRESENTATION ( '', ( #36189, #12375 ), #43820 ) ;
#15626=VECTOR ( 'NONE', #17526, 1000.000000000000114 ) ;
#15647=FACE_OUTER_BOUND ( 'NONE', #15108, .T. ) ;
#15652=EDGE_CURVE ( 'NONE', #44020, #17452, #34395, .T. ) ;
#15653=PRODUCT_DEFINITION ( 'UNKNOWN', '', #917, #42913 ) ;
#15657=VERTEX_POINT ( 'NONE', #9636 ) ;
#15670=ORIENTED_EDGE ( 'NONE', *, *, #10288, .F. ) ;
#15671=DIRECTION ( 'NONE',  ( 1.000000000000000000, 0.000000000000000000, 0.000000000000000000 ) ) ;
#15688=EDGE_LOOP ( 'NONE', ( #13904, #17743, #16501, #19880, #40440, #22359 ) ) ;
#15700=CARTESIAN_POINT ( 'NONE',  ( 91.77400275106518279, -25.99489077589524300, -13.39321520033831625 ) ) ;
#15702=ORIENTED_EDGE ( 'NONE', *, *, #20863, .F. ) ;
#15708=EDGE_LOOP ( 'NONE', ( #38255, #6969, #31767, #20987, #40709 ) ) ;
#15719=EDGE_CURVE ( 'NONE', #2333, #33578, #9405, .T. ) ;
#15728=ORIENTED_EDGE ( 'NONE', *, *, #27901, .T. ) ;
#15730=DIRECTION ( 'NONE',  ( 0.000000000000000000, 0.3818493186865928868, -0.9242245927363028635 ) ) ;
#15762=CARTESIAN_POINT ( 'NONE',  ( 85.70478001548416103, -27.84333996136784961, -14.15691383771150136 ) ) ;
#15797=ORIENTED_EDGE ( 'NONE', *, *, #301, .F. ) ;
#15814=AXIS2_PLACEMENT_3D ( 'NONE', #43499, #12713, #33207 ) ;
#15827=CIRCLE ( 'NONE', #31114, 2.000000000000000444 ) ;
#15838=VECTOR ( 'NONE', #18148, 1000.000000000000000 ) ;
#15844=DIRECTION ( 'NONE',  ( 0.000000000000000000, -0.3818493186865927203, 0.9242245927363029745 ) ) ;
#15860=CARTESIAN_POINT ( 'NONE',  ( 94.86797725101187950, -26.47803208098435945, -14.15005199485239906 ) ) ;
#15871=DIRECTION ( 'NONE',  ( 1.000000000000000000, 0.000000000000000000, -0.000000000000000000 ) ) ;
#15899=EDGE_CURVE ( 'NONE', #12976, #37160, #10101, .T. ) ;
#15902=CARTESIAN_POINT ( 'NONE',  ( 87.14323352029596492, -25.23119213852205789, -15.24166438581092109 ) ) ;
#15905=VECTOR ( 'NONE', #20526, 1000.000000000000114 ) ;
#15931=ORIENTED_EDGE ( 'NONE', *, *, #19759, .F. ) ;
#15957=DIRECTION ( 'NONE',  ( 0.000000000000000000, -0.3818493186865936084, 0.9242245927363024194 ) ) ;
#15972=ORIENTED_EDGE ( 'NONE', *, *, #9728, .F. ) ;
#15988=ORIENTED_EDGE ( 'NONE', *, *, #34509, .T. ) ;
#15999=AXIS2_PLACEMENT_3D ( 'NONE', #36611, #5386, #19303 ) ;
#16007=EDGE_LOOP ( 'NONE', ( #14082, #329, #42972, #44580, #30344 ) ) ;
#16008=EDGE_LOOP ( 'NONE', ( #20768, #26301, #23818, #34454, #4726 ) ) ;
#16022=VERTEX_POINT ( 'NONE', #35802 ) ;
#16025=CARTESIAN_POINT ( 'NONE',  ( 85.82015659721905365, -25.23119213852205789, -15.24166438581092109 ) ) ;
#16029=AXIS2_PLACEMENT_3D ( 'NONE', #29880, #19848, #26467 ) ;
#16031=ORIENTED_EDGE ( 'NONE', *, *, #7485, .F. ) ;
#16061=AXIS2_PLACEMENT_3D ( 'NONE', #31841, #7222, #21135 ) ;
#16079=DIRECTION ( 'NONE',  ( 1.000000000000000000, 0.000000000000000000, -0.000000000000000000 ) ) ;
#16091=DIRECTION ( 'NONE',  ( 0.000000000000000000, -0.3818493186865927203, 0.9242245927363029745 ) ) ;
#16097=EDGE_CURVE ( 'NONE', #24723, #5058, #42890, .T. ) ;
#16129=EDGE_CURVE ( 'NONE', #5448, #14305, #35098, .T. ) ;
#16142=B_SPLINE_CURVE_WITH_KNOTS ( 'NONE', 3,
 ( #25368, #21936, #35375, #18964 ),
 .UNSPECIFIED., .F., .F.,
 ( 4, 4 ),
 ( 0.000000000000000000, 1.000000000000000000 ),
 .UNSPECIFIED. ) ;
#16163=DIRECTION ( 'NONE',  ( 0.000000000000000000, 0.3818493186865927203, -0.9242245927363029745 ) ) ;
#16190=AXIS2_PLACEMENT_3D ( 'NONE', #44649, #13411, #10211 ) ;
#16201=EDGE_LOOP ( 'NONE', ( #3815, #10712, #26968, #21041, #32970 ) ) ;
#16205=VECTOR ( 'NONE', #14097, 1000.000000000000000 ) ;
#16212=CYLINDRICAL_SURFACE ( 'NONE', #33618, 1.999999999999998890 ) ;
#16244=( NAMED_UNIT ( * ) PLANE_ANGLE_UNIT ( ) SI_UNIT ( $, .RADIAN. ) );
#16274=DIRECTION ( 'NONE',  ( -0.4461977533474357771, -0.3417300876246960328, 0.8271203734159368048 ) ) ;
#16275=CARTESIAN_POINT ( 'NONE',  ( 85.70478001548416103, -25.99489077589524300, -13.39321520033831447 ) ) ;
#16281=DIRECTION ( 'NONE',  ( 1.000000000000000000, 0.000000000000000000, -0.000000000000000000 ) ) ;
#16285=ORIENTED_EDGE ( 'NONE', *, *, #16097, .F. ) ;
#16294=EDGE_CURVE ( 'NONE', #44020, #23032, #16958, .T. ) ;
#16345=CARTESIAN_POINT ( 'NONE',  ( 90.45092582798827152, -25.99489077589524300, -13.39321520033831625 ) ) ;
#16356=EDGE_CURVE ( 'NONE', #17364, #13419, #21290, .T. ) ;
#16373=AXIS2_PLACEMENT_3D ( 'NONE', #4002, #20688, #17924 ) ;
#16383=ORIENTED_EDGE ( 'NONE', *, *, #32967, .F. ) ;
#16387=EDGE_CURVE ( 'NONE', #43753, #38363, #27850, .T. ) ;
#16395=EDGE_CURVE ( 'NONE', #9155, #7716, #5335, .T. ) ;
#16407=VERTEX_POINT ( 'NONE', #35467 ) ;
#16411=EDGE_CURVE ( 'NONE', #21347, #37027, #33643, .T. ) ;
#16414=EDGE_CURVE ( 'NONE', #30603, #31353, #7664, .T. ) ;
#16432=CARTESIAN_POINT ( 'NONE',  ( 90.06246830635160450, -25.38011337280982715, -14.88121679464376257 ) ) ;
#16458=ORIENTED_EDGE ( 'NONE', *, *, #28971, .T. ) ;
#16501=ORIENTED_EDGE ( 'NONE', *, *, #24355, .T. ) ;
#16502=DIRECTION ( 'NONE',  ( 1.000000000000000000, 0.000000000000000000, -0.000000000000000000 ) ) ;
#16503=LINE ( 'NONE', #23335, #13609 ) ;
#16521=CIRCLE ( 'NONE', #19427, 2.000000000000000444 ) ;
#16532=CARTESIAN_POINT ( 'NONE',  ( 94.20708369096698220, -25.99489077589524300, -13.39321520033831447 ) ) ;
#16537=CARTESIAN_POINT ( 'NONE',  ( 121.9470836909669913, -25.99489077589524300, -13.39321520033831447 ) ) ;
#16542=CARTESIAN_POINT ( 'NONE',  ( 89.01247232317646763, -27.84333996136784961, -14.15691383771150136 ) ) ;
#16590=DIRECTION ( 'NONE',  ( 0.000000000000000000, 0.3818493186865927203, -0.9242245927363029745 ) ) ;
#16594=VECTOR ( 'NONE', #24042, 1000.000000000000000 ) ;
#16614=DIRECTION ( 'NONE',  ( 1.000000000000000000, 0.000000000000000000, -0.000000000000000000 ) ) ;
#16628=VECTOR ( 'NONE', #38730, 1000.000000000000114 ) ;
#16631=EDGE_LOOP ( 'NONE', ( #9317, #37647, #37655, #1066, #19423 ) ) ;
#16641=CARTESIAN_POINT ( 'NONE',  ( 90.45092582798827152, -25.99489077589524300, -13.39321520033831625 ) ) ;
#16645=PLANE ( 'NONE',  #26687 ) ;
#16663=CARTESIAN_POINT ( 'NONE',  ( 94.20708369096698220, -24.88943055980569241, -13.49371108670732333 ) ) ;
#16669=ORIENTED_EDGE ( 'NONE', *, *, #40084, .T. ) ;
#16677=DIRECTION ( 'NONE',  ( 0.000000000000000000, -0.3818493186865936084, 0.9242245927363024194 ) ) ;
#16694=ORIENTED_EDGE ( 'NONE', *, *, #30585, .F. ) ;
#16701=EDGE_CURVE ( 'NONE', #15443, #24220, #20647, .T. ) ;
#16730=DIRECTION ( 'NONE',  ( 1.000000000000000000, 0.000000000000000000, -0.000000000000000000 ) ) ;
#16737=AXIS2_PLACEMENT_3D ( 'NONE', #42279, #14015, #38172 ) ;
#16747=ORIENTED_EDGE ( 'NONE', *, *, #13998, .F. ) ;
#16822=CIRCLE ( 'NONE', #35731, 2.000000000000000444 ) ;
#16836=AXIS2_PLACEMENT_3D ( 'NONE', #41003, #6553, #34351 ) ;
#16840=ORIENTED_EDGE ( 'NONE', *, *, #41810, .T. ) ;
#16841=AXIS2_PLACEMENT_3D ( 'NONE', #43781, #37135, #19152 ) ;
#16859=AXIS2_PLACEMENT_3D ( 'NONE', #33226, #36206, #26181 ) ;
#16874=DIRECTION ( 'NONE',  ( 1.000000000000000000, 0.000000000000000000, -0.000000000000000000 ) ) ;
#16876=LINE ( 'NONE', #13000, #43420 ) ;
#16884=ORIENTED_EDGE ( 'NONE', *, *, #13360, .T. ) ;
#16899=CARTESIAN_POINT ( 'NONE',  ( 91.11246428952674137, -25.23119213852205789, -15.24166438581092109 ) ) ;
#16907=DIRECTION ( 'NONE',  ( 0.5735764363510499342, 0.3127926500124801890, -0.7570804645221008711 ) ) ;
#16920=ORIENTED_EDGE ( 'NONE', *, *, #19432, .F. ) ;
#16921=ORIENTED_EDGE ( 'NONE', *, *, #28963, .T. ) ;
#16934=EDGE_CURVE ( 'NONE', #5517, #9582, #44652, .T. ) ;
#16935=ORIENTED_EDGE ( 'NONE', *, *, #27338, .T. ) ;
#16948=CARTESIAN_POINT ( 'NONE',  ( 91.38554522942851577, -25.38011337280982715, -14.88121679464376257 ) ) ;
#16958=CIRCLE ( 'NONE', #16190, 3.853420195439741125 ) ;
#16967=EDGE_CURVE ( 'NONE', #14657, #8089, #12341, .T. ) ;
#16971=CARTESIAN_POINT ( 'NONE',  ( 121.9470836909669913, -24.14644159042263993, -12.62951656296512937 ) ) ;
#16976=EDGE_LOOP ( 'NONE', ( #43388, #29988, #42955, #4406, #27823 ) ) ;
#16988=EDGE_CURVE ( 'NONE', #12295, #27606, #32228, .T. ) ;
#16993=ADVANCED_FACE ( 'NONE', ( #10605 ), #33676, .T. ) ;
#16997=CARTESIAN_POINT ( 'NONE',  ( 83.44708369096697709, -25.38011337280982715, -14.88121679464376257 ) ) ;
#17008=DIRECTION ( 'NONE',  ( 1.000000000000000000, 0.000000000000000000, -0.000000000000000000 ) ) ;
#17031=TOROIDAL_SURFACE ( 'NONE', #38833, 3.640000000000000124, 0.3600000000000000422 ) ;
#17035=ORIENTED_EDGE ( 'NONE', *, *, #34209, .F. ) ;
#17038=EDGE_CURVE ( 'NONE', #12295, #19939, #6019, .T. ) ;
#17039=CARTESIAN_POINT ( 'NONE',  ( 88.07785292173620917, -25.38011337280982715, -14.88121679464376257 ) ) ;
#17044=FACE_OUTER_BOUND ( 'NONE', #21970, .T. ) ;
#17047=DIRECTION ( 'NONE',  ( 1.000000000000000000, 0.000000000000000000, -0.000000000000000000 ) ) ;
#17050=ORIENTED_EDGE ( 'NONE', *, *, #5225, .T. ) ;
#17051=CARTESIAN_POINT ( 'NONE',  ( 85.82015659721905365, -25.99489077589524300, -13.39321520033831625 ) ) ;
#17052=ADVANCED_FACE ( 'NONE', ( #35185 ), #18334, .T. ) ;
#17054=DIRECTION ( 'NONE',  ( 1.000000000000000000, 0.000000000000000000, -0.000000000000000000 ) ) ;
#17065=ORIENTED_EDGE ( 'NONE', *, *, #34209, .T. ) ;
#17090=EDGE_LOOP ( 'NONE', ( #43539, #5028, #3168, #72, #10155 ) ) ;
#17134=AXIS2_PLACEMENT_3D ( 'NONE', #21447, #35332, #18023 ) ;
#17146=ORIENTED_EDGE ( 'NONE', *, *, #3118, .T. ) ;
#17158=DIRECTION ( 'NONE',  ( 0.000000000000000000, -0.9242245927363026414, -0.3818493186865934419 ) ) ;
#17171=DIRECTION ( 'NONE',  ( 1.000000000000000000, 0.000000000000000000, -0.000000000000000000 ) ) ;
#17218=EDGE_LOOP ( 'NONE', ( #8290, #8184, #33051, #7811, #23040 ) ) ;
#17255=DIRECTION ( 'NONE',  ( 0.000000000000000000, -0.3818493186865936084, 0.9242245927363024194 ) ) ;
#17264=CIRCLE ( 'NONE', #25261, 0.3599999999999998201 ) ;
#17278=DIRECTION ( 'NONE',  ( 1.000000000000000000, 0.000000000000000000, -0.000000000000000000 ) ) ;
#17314=CARTESIAN_POINT ( 'NONE',  ( 121.9470836909669913, -27.84333996136784961, -14.15691383771150136 ) ) ;
#17328=DIRECTION ( 'NONE',  ( 1.000000000000000000, 0.000000000000000000, -0.000000000000000000 ) ) ;
#17351=ORIENTED_EDGE ( 'NONE', *, *, #2823, .F. ) ;
#17364=VERTEX_POINT ( 'NONE', #28265 ) ;
#17368=DIRECTION ( 'NONE',  ( 1.000000000000000000, 0.000000000000000000, -0.000000000000000000 ) ) ;
#17371=AXIS2_PLACEMENT_3D ( 'NONE', #206, #14120, #35062 ) ;
#17385=ORIENTED_EDGE ( 'NONE', *, *, #1363, .F. ) ;
#17412=ORIENTED_EDGE ( 'NONE', *, *, #14261, .F. ) ;
#17452=VERTEX_POINT ( 'NONE', #12856 ) ;
#17457=VERTEX_POINT ( 'NONE', #44092 ) ;
#17462=ORIENTED_EDGE ( 'NONE', *, *, #21558, .T. ) ;
#17465=LINE ( 'NONE', #10192, #5806 ) ;
#17476=CARTESIAN_POINT ( 'NONE',  ( 87.14323352029596492, -26.75858941326842810, -11.54476601486570964 ) ) ;
#17482=CARTESIAN_POINT ( 'NONE',  ( 89.78938736644981589, -25.99489077589524300, -13.39321520033831625 ) ) ;
#17511=DIRECTION ( 'NONE',  ( 1.000000000000000000, 0.000000000000000000, -0.000000000000000000 ) ) ;
#17516=EDGE_CURVE ( 'NONE', #12241, #24220, #18437, .T. ) ;
#17526=DIRECTION ( 'NONE',  ( 0.3090169943749414005, 0.8789898214420971412, 0.3631602827797495991 ) ) ;
#17529=AXIS2_PLACEMENT_3D ( 'NONE', #6962, #41633, #37968 ) ;
#17540=ORIENTED_EDGE ( 'NONE', *, *, #3588, .F. ) ;
#17543=DIRECTION ( 'NONE',  ( 0.000000000000000000, -0.3818493186865927203, 0.9242245927363029745 ) ) ;
#17547=ORIENTED_EDGE ( 'NONE', *, *, #41198, .T. ) ;
#17568=DIRECTION ( 'NONE',  ( 1.000000000000000000, 0.000000000000000000, -0.000000000000000000 ) ) ;
#17582=CARTESIAN_POINT ( 'NONE',  ( 90.99708770779186295, -25.99489077589524300, -13.39321520033831447 ) ) ;
#17588=CIRCLE ( 'NONE', #19044, 0.8509999999999994236 ) ;
#17608=ADVANCED_FACE ( 'NONE', ( #42397 ), #1110, .T. ) ;
#17626=DIRECTION ( 'NONE',  ( 0.000000000000000000, -0.3818493186865897226, 0.9242245927363041957 ) ) ;
#17628=VERTEX_POINT ( 'NONE', #4070 ) ;
#17635=CARTESIAN_POINT ( 'NONE',  ( 121.9470836909669913, -27.84333996136784961, -14.15691383771150136 ) ) ;
#17646=VERTEX_POINT ( 'NONE', #32343 ) ;
#17648=AXIS2_PLACEMENT_3D ( 'NONE', #8023, #14419, #42241 ) ;
#17651=DIRECTION ( 'NONE',  ( 1.000000000000000000, 0.000000000000000000, -0.000000000000000000 ) ) ;
#17652=SPHERICAL_SURFACE ( 'NONE', #23990, 6.500000000000000000 ) ;
#17673=DIRECTION ( 'NONE',  ( 1.000000000000000000, 0.000000000000000000, -0.000000000000000000 ) ) ;
#17684=CIRCLE ( 'NONE', #43887, 2.000000000000000444 ) ;
#17689=DIRECTION ( 'NONE',  ( 1.000000000000000000, 0.000000000000000000, -0.000000000000000000 ) ) ;
#17700=DIRECTION ( 'NONE',  ( 1.000000000000000000, 0.000000000000000000, -0.000000000000000000 ) ) ;
#17718=DIRECTION ( 'NONE',  ( 0.000000000000000000, 0.3818493186865927203, -0.9242245927363029745 ) ) ;
#17727=CARTESIAN_POINT ( 'NONE',  ( 83.72016463086879412, -24.14644159042263993, -12.62951656296512937 ) ) ;
#17737=ORIENTED_EDGE ( 'NONE', *, *, #35637, .F. ) ;
#17741=FACE_OUTER_BOUND ( 'NONE', #17090, .T. ) ;
#17743=ORIENTED_EDGE ( 'NONE', *, *, #902, .T. ) ;
#17746=CARTESIAN_POINT ( 'NONE',  ( 84.77016061404391678, -25.99489077589524300, -13.39321520033831625 ) ) ;
#17757=DIRECTION ( 'NONE',  ( 0.000000000000000000, -0.3818493186865927203, 0.9242245927363029745 ) ) ;
#17775=EDGE_CURVE ( 'NONE', #2572, #4353, #35891, .T. ) ;
#17790=DIRECTION ( 'NONE',  ( -0.000000000000000000, -0.3818493186865893341, 0.9242245927363043068 ) ) ;
#17814=FACE_OUTER_BOUND ( 'NONE', #2784, .T. ) ;
#17823=ORIENTED_EDGE ( 'NONE', *, *, #9728, .T. ) ;
#17849=ORIENTED_EDGE ( 'NONE', *, *, #36785, .F. ) ;
#17851=EDGE_CURVE ( 'NONE', #2333, #35973, #10889, .T. ) ;
#17864=AXIS2_PLACEMENT_3D ( 'NONE', #29581, #22069, #11585 ) ;
#17884=CARTESIAN_POINT ( 'NONE',  ( 90.45092582798827152, -26.75858941326842810, -11.54476601486570964 ) ) ;
#17887=DIRECTION ( 'NONE',  ( 1.000000000000000000, 0.000000000000000000, -0.000000000000000000 ) ) ;
#17912=CARTESIAN_POINT ( 'NONE',  ( 89.78938736644981589, -25.99489077589524300, -13.39321520033831625 ) ) ;
#17924=DIRECTION ( 'NONE',  ( 0.000000000000000000, -0.3818493186865927203, 0.9242245927363029745 ) ) ;
#17950=DIRECTION ( 'NONE',  ( 1.000000000000000000, 0.000000000000000000, -0.000000000000000000 ) ) ;
#17954=AXIS2_PLACEMENT_3D ( 'NONE', #29665, #1394, #40158 ) ;
#17960=DIRECTION ( 'NONE',  ( 0.000000000000000000, -0.9242245927363029745, -0.3818493186865927203 ) ) ;
#17966=ORIENTED_EDGE ( 'NONE', *, *, #23045, .T. ) ;
#17975=CARTESIAN_POINT ( 'NONE',  ( 85.82015659721905365, -25.99489077589524300, -13.39321520033831625 ) ) ;
#17986=CONICAL_SURFACE ( 'NONE', #21602, 0.8509999999999994236, 0.06981317007976593769 ) ;
#17988=CYLINDRICAL_SURFACE ( 'NONE', #29830, 1.999999999999998890 ) ;
#18018=DIRECTION ( 'NONE',  ( 1.000000000000000000, 0.000000000000000000, -0.000000000000000000 ) ) ;
#18023=DIRECTION ( 'NONE',  ( 0.000000000000000000, -0.3818493186865936084, 0.9242245927363024194 ) ) ;
#18024=CIRCLE ( 'NONE', #4899, 0.1999999999999988731 ) ;
#18037=VERTEX_POINT ( 'NONE', #16997 ) ;
#18039=DIRECTION ( 'NONE',  ( 0.000000000000000000, -0.3818493186865927203, 0.9242245927363029745 ) ) ;
#18044=CIRCLE ( 'NONE', #5629, 6.479565957685750277 ) ;
#18047=ORIENTED_EDGE ( 'NONE', *, *, #2756, .F. ) ;
#18048=EDGE_CURVE ( 'NONE', #16022, #10767, #14822, .T. ) ;
#18054=ADVANCED_FACE ( 'NONE', ( #37950 ), #40302, .T. ) ;
#18073=FACE_OUTER_BOUND ( 'NONE', #33737, .T. ) ;
#18105=EDGE_CURVE ( 'NONE', #28442, #9192, #38825, .T. ) ;
#18109=DIRECTION ( 'NONE',  ( 0.000000000000000000, -0.3818493186865936084, 0.9242245927363024194 ) ) ;
#18112=CARTESIAN_POINT ( 'NONE',  ( 121.9470836909669913, -24.14644159042263993, -12.62951656296512937 ) ) ;
#18118=FACE_OUTER_BOUND ( 'NONE', #2702, .T. ) ;
#18147=DIRECTION ( 'NONE',  ( 1.000000000000000000, 0.000000000000000000, -0.000000000000000000 ) ) ;
#18148=DIRECTION ( 'NONE',  ( -0.8949343913984425525, 0.1703803081152066579, -0.4123869368673873104 ) ) ;
#18176=CIRCLE ( 'NONE', #26933, 2.000000000000000444 ) ;
#18201=DIRECTION ( 'NONE',  ( -1.000000000000000000, 0.000000000000000000, 0.000000000000000000 ) ) ;
#18213=CONICAL_SURFACE ( 'NONE', #43705, 1.610000000000000986, 0.9599310885968765916 ) ;
#18226=ORIENTED_EDGE ( 'NONE', *, *, #3885, .F. ) ;
#18235=DIRECTION ( 'NONE',  ( 1.000000000000000000, 0.000000000000000000, -0.000000000000000000 ) ) ;
#18238=DIRECTION ( 'NONE',  ( 1.000000000000000000, 0.000000000000000000, -0.000000000000000000 ) ) ;
#18240=EDGE_CURVE ( 'NONE', #21444, #41351, #27197, .T. ) ;
#18243=ORIENTED_EDGE ( 'NONE', *, *, #6936, .F. ) ;
#18248=ORIENTED_EDGE ( 'NONE', *, *, #40084, .F. ) ;
#18249=AXIS2_PLACEMENT_3D ( 'NONE', #31569, #39985, #29499 ) ;
#18251=LINE ( 'NONE', #29182, #13930 ) ;
#18267=DIRECTION ( 'NONE',  ( 1.000000000000000000, 0.000000000000000000, -0.000000000000000000 ) ) ;
#18284=CARTESIAN_POINT ( 'NONE',  ( 121.9470836909669913, -25.99489077589524300, -13.39321520033831447 ) ) ;
#18292=ORIENTED_EDGE ( 'NONE', *, *, #8110, .T. ) ;
#18316=PRODUCT_DEFINITION_SHAPE ( 'NONE', 'NONE',  #15653 ) ;
#18321=ORIENTED_EDGE ( 'NONE', *, *, #8072, .T. ) ;
#18324=DIRECTION ( 'NONE',  ( 1.000000000000000000, 0.000000000000000000, -0.000000000000000000 ) ) ;
#18325=CARTESIAN_POINT ( 'NONE',  ( 121.9470836909669913, -25.99489077589524300, -13.39321520033831447 ) ) ;
#18327=EDGE_LOOP ( 'NONE', ( #40806, #39896, #3048, #15797, #22365 ) ) ;
#18334=CYLINDRICAL_SURFACE ( 'NONE', #7477, 1.999999999999998890 ) ;
#18336=ADVANCED_FACE ( 'NONE', ( #32609 ), #26482, .T. ) ;
#18337=VERTEX_POINT ( 'NONE', #11879 ) ;
#18343=DIRECTION ( 'NONE',  ( 0.000000000000000000, -0.3818493186865927203, 0.9242245927363029745 ) ) ;
#18354=CIRCLE ( 'NONE', #43838, 6.500000000000005329 ) ;
#18364=ADVANCED_FACE ( 'NONE', ( #42511 ), #232, .T. ) ;
#18366=EDGE_CURVE ( 'NONE', #24723, #2572, #24948, .T. ) ;
#18396=DIRECTION ( 'NONE',  ( 1.000000000000000000, 0.000000000000000000, -0.000000000000000000 ) ) ;
#18420=CARTESIAN_POINT ( 'NONE',  ( 83.72016463086879412, -25.99489077589524300, -13.39321520033831447 ) ) ;
#18434=CYLINDRICAL_SURFACE ( 'NONE', #41141, 1.999999999999998890 ) ;
#18437=CIRCLE ( 'NONE', #35166, 2.000000000000000444 ) ;
#18445=ORIENTED_EDGE ( 'NONE', *, *, #3885, .T. ) ;
#18449=CONICAL_SURFACE ( 'NONE', #10449, 1.610000000000000986, 0.9599310885968765916 ) ;
#18467=DIRECTION ( 'NONE',  ( -0.5735764363510450492, -0.3127926500124816878, 0.7570804645221038687 ) ) ;
#18488=FACE_OUTER_BOUND ( 'NONE', #23538, .T. ) ;
#18502=ORIENTED_EDGE ( 'NONE', *, *, #2285, .T. ) ;
#18512=ORIENTED_EDGE ( 'NONE', *, *, #15069, .T. ) ;
#18522=LINE ( 'NONE', #14878, #22224 ) ;
#18547=VECTOR ( 'NONE', #139, 999.9999999999998863 ) ;
#18554=CARTESIAN_POINT ( 'NONE',  ( 92.32016463086877422, -25.99489077589524300, -13.39321520033831447 ) ) ;
#18559=CIRCLE ( 'NONE', #9092, 0.8509999999999994236 ) ;
#18612=CIRCLE ( 'NONE', #17864, 2.000000000000000444 ) ;
#18621=CARTESIAN_POINT ( 'NONE',  ( 94.20708369096698220, -25.77760949922539879, -12.57042127303408385 ) ) ;
#18644=ORIENTED_EDGE ( 'NONE', *, *, #20054, .F. ) ;
#18662=CARTESIAN_POINT ( 'NONE',  ( 121.9470836909669913, -24.14644159042263993, -12.62951656296512937 ) ) ;
#18672=VERTEX_POINT ( 'NONE', #2800 ) ;
#18684=CARTESIAN_POINT ( 'NONE',  ( 90.06246830635160450, -25.99489077589524300, -13.39321520033831625 ) ) ;
#18687=CARTESIAN_POINT ( 'NONE',  ( 90.04708369096697140, -26.47086644115443832, -13.58986759946190936 ) ) ;
#18703=DIRECTION ( 'NONE',  ( -1.000000000000000000, 0.000000000000000000, 0.000000000000000000 ) ) ;
#18708=CARTESIAN_POINT ( 'NONE',  ( 90.45092582798827152, -27.84333996136784961, -14.15691383771150136 ) ) ;
#18709=DIRECTION ( 'NONE',  ( -0.8949343913984423304, 0.1703803081152067689, -0.4123869368673877545 ) ) ;
#18722=DIRECTION ( 'NONE',  ( 0.000000000000000000, -0.3818493186865936084, 0.9242245927363024194 ) ) ;
#18727=FACE_OUTER_BOUND ( 'NONE', #30156, .T. ) ;
#18735=DIRECTION ( 'NONE',  ( -0.4461977533474357216, 0.8271203734159378040, 0.3417300876246930907 ) ) ;
#18746=DIRECTION ( 'NONE',  ( 1.000000000000000000, 0.000000000000000000, -0.000000000000000000 ) ) ;
#18772=CARTESIAN_POINT ( 'NONE',  ( 85.15861813568058380, -25.99489077589524300, -13.39321520033831625 ) ) ;
#18779=CARTESIAN_POINT ( 'NONE',  ( 90.72400676789006013, -26.60966817898065884, -11.90521360603286816 ) ) ;
#18786=ORIENTED_EDGE ( 'NONE', *, *, #28523, .T. ) ;
#18813=CARTESIAN_POINT ( 'NONE',  ( 95.28169473643895060, -22.43346506512310512, -11.92178932409649228 ) ) ;
#18817=DIRECTION ( 'NONE',  ( 0.000000000000000000, -0.9242245927363027524, -0.3818493186865929423 ) ) ;
#18837=DIRECTION ( 'NONE',  ( 0.000000000000000000, -0.3818493186865936084, 0.9242245927363024194 ) ) ;
#18889=AXIS2_PLACEMENT_3D ( 'NONE', #14678, #7603, #38599 ) ;
#18891=CARTESIAN_POINT ( 'NONE',  ( 94.20708369096698220, -25.14343533174585943, -14.10537061818067883 ) ) ;
#18922=ADVANCED_FACE ( 'NONE', ( #7332 ), #21251, .T. ) ;
#18926=PLANE ( 'NONE',  #64 ) ;
#18934=DIRECTION ( 'NONE',  ( 1.000000000000000000, 0.000000000000000000, -0.000000000000000000 ) ) ;
#18945=DIRECTION ( 'NONE',  ( -1.000000000000000000, 0.000000000000000000, 0.000000000000000000 ) ) ;
#18948=CARTESIAN_POINT ( 'NONE',  ( 89.12784890491134604, -25.99489077589524300, -13.39321520033831625 ) ) ;
#18956=VECTOR ( 'NONE', #27321, 1000.000000000000114 ) ;
#18963=CIRCLE ( 'NONE', #42246, 2.000000000000000444 ) ;
#18964=CARTESIAN_POINT ( 'NONE',  ( 96.46827370896536991, -24.99618726903056753, -13.53781830588664903 ) ) ;
#18974=EDGE_LOOP ( 'NONE', ( #1991, #33150, #34587, #13389, #35032 ) ) ;
#18977=ORIENTED_EDGE ( 'NONE', *, *, #24470, .F. ) ;
#18998=DIRECTION ( 'NONE',  ( 7.002829358989538952E-15, -0.3818493186865928868, 0.9242245927363027524 ) ) ;
#19018=VECTOR ( 'NONE', #7720, 1000.000000000000000 ) ;
#19024=AXIS2_PLACEMENT_3D ( 'NONE', #6327, #41227, #31164 ) ;
#19032=EDGE_CURVE ( 'NONE', #19992, #18672, #35205, .T. ) ;
#19044=AXIS2_PLACEMENT_3D ( 'NONE', #16532, #34721, #30879 ) ;
#19058=CONICAL_SURFACE ( 'NONE', #43810, 2.000000000000000444, 0.9599310885968830309 ) ;
#19061=DIRECTION ( 'NONE',  ( -1.000000000000000000, 0.000000000000000000, 0.000000000000000000 ) ) ;
#19084=ORIENTED_EDGE ( 'NONE', *, *, #3556, .F. ) ;
#19090=EDGE_CURVE ( 'NONE', #42815, #44289, #23590, .T. ) ;
#19113=DIRECTION ( 'NONE',  ( -1.000000000000000000, 0.000000000000000000, 0.000000000000000000 ) ) ;
#19143=EDGE_LOOP ( 'NONE', ( #36097, #37751, #5601, #5482, #43808 ) ) ;
#19152=DIRECTION ( 'NONE',  ( 0.000000000000000000, -0.3818493186865927203, 0.9242245927363029745 ) ) ;
#19159=DIRECTION ( 'NONE',  ( 0.000000000000000000, 0.3818493186865927203, -0.9242245927363029745 ) ) ;
#19161=ADVANCED_FACE ( 'NONE', ( #21484 ), #508, .T. ) ;
#19169=CARTESIAN_POINT ( 'NONE',  ( 86.09323753712084226, -25.99489077589524300, -13.39321520033831625 ) ) ;
#19177=EDGE_CURVE ( 'NONE', #39489, #12241, #8695, .T. ) ;
#19181=ORIENTED_EDGE ( 'NONE', *, *, #7719, .F. ) ;
#19195=CIRCLE ( 'NONE', #11190, 0.8509999999999994236 ) ;
#19198=VERTEX_POINT ( 'NONE', #29671 ) ;
#19208=ORIENTED_EDGE ( 'NONE', *, *, #1346, .F. ) ;
#19210=DIRECTION ( 'NONE',  ( 1.000000000000000000, 0.000000000000000000, -0.000000000000000000 ) ) ;
#19227=ORIENTED_EDGE ( 'NONE', *, *, #35637, .T. ) ;
#19262=DIRECTION ( 'NONE',  ( 1.000000000000000000, 0.000000000000000000, -0.000000000000000000 ) ) ;
#19271=ORIENTED_EDGE ( 'NONE', *, *, #22576, .T. ) ;
#19276=DIRECTION ( 'NONE',  ( 0.000000000000000000, -0.9242245927363026414, -0.3818493186865934419 ) ) ;
#19291=DIRECTION ( 'NONE',  ( 0.000000000000000000, -0.9242245927363027524, -0.3818493186865929978 ) ) ;
#19293=PLANE ( 'NONE',  #2988 ) ;
#19303=DIRECTION ( 'NONE',  ( -1.000000000000000000, 0.000000000000000000, 0.000000000000000000 ) ) ;
#19314=CARTESIAN_POINT ( 'NONE',  ( 121.9470836909669913, -27.84333996136784961, -14.15691383771150136 ) ) ;
#19322=CARTESIAN_POINT ( 'NONE',  ( 94.20708369096698220, -26.72956082974378944, -12.96372607128127363 ) ) ;
#19325=DIRECTION ( 'NONE',  ( 1.000000000000000000, 0.000000000000000000, -0.000000000000000000 ) ) ;
#19349=ORIENTED_EDGE ( 'NONE', *, *, #38190, .F. ) ;
#19363=VERTEX_POINT ( 'NONE', #13030 ) ;
#19372=CARTESIAN_POINT ( 'NONE',  ( 93.24708369096698846, -25.99489077589524300, -13.39321520033831447 ) ) ;
#19377=AXIS2_PLACEMENT_3D ( 'NONE', #20151, #6229, #26980 ) ;
#19392=ORIENTED_EDGE ( 'NONE', *, *, #32712, .T. ) ;
#19413=CIRCLE ( 'NONE', #12888, 2.000000000000000444 ) ;
#19421=CIRCLE ( 'NONE', #36171, 1.610000000000000986 ) ;
#19423=ORIENTED_EDGE ( 'NONE', *, *, #20879, .F. ) ;
#19426=CARTESIAN_POINT ( 'NONE',  ( 94.20708369096698220, -25.89439488952623591, -12.28775498424876211 ) ) ;
#19427=AXIS2_PLACEMENT_3D ( 'NONE', #33029, #39451, #22344 ) ;
#19430=CARTESIAN_POINT ( 'NONE',  ( 90.48265143217095385, -26.32847964148556485, -12.58579976615069818 ) ) ;
#19432=EDGE_CURVE ( 'NONE', #44761, #23032, #30125, .T. ) ;
#19438=EDGE_CURVE ( 'NONE', #2933, #8919, #34645, .T. ) ;
#19446=ORIENTED_EDGE ( 'NONE', *, *, #28153, .T. ) ;
#19454=AXIS2_PLACEMENT_3D ( 'NONE', #36854, #27069, #37076 ) ;
#19479=AXIS2_PLACEMENT_3D ( 'NONE', #12390, #22636, #1874 ) ;
#19485=DIRECTION ( 'NONE',  ( 0.000000000000000000, -0.9242245927363027524, -0.3818493186865928868 ) ) ;
#19486=EDGE_CURVE ( 'NONE', #8919, #14657, #31018, .T. ) ;
#19492=EDGE_CURVE ( 'NONE', #19939, #22843, #10070, .T. ) ;
#19493=ORIENTED_EDGE ( 'NONE', *, *, #8377, .T. ) ;
#19513=CARTESIAN_POINT ( 'NONE',  ( 89.12784890491134604, -25.99489077589524300, -13.39321520033831625 ) ) ;
#19531=VERTEX_POINT ( 'NONE', #23971 ) ;
#19537=DIRECTION ( 'NONE',  ( 1.000000000000000000, 0.000000000000000000, -0.000000000000000000 ) ) ;
#19542=DIRECTION ( 'NONE',  ( -0.000000000000000000, -0.9242245927363028635, -0.3818493186865929423 ) ) ;
#19543=AXIS2_PLACEMENT_3D ( 'NONE', #44663, #10225, #30740 ) ;
#19553=ORIENTED_EDGE ( 'NONE', *, *, #3091, .T. ) ;
#19585=CYLINDRICAL_SURFACE ( 'NONE', #15543, 1.999999999999998890 ) ;
#19592=ORIENTED_EDGE ( 'NONE', *, *, #11107, .F. ) ;
#19629=EDGE_CURVE ( 'NONE', #5448, #14958, #29653, .T. ) ;
#19639=ORIENTED_EDGE ( 'NONE', *, *, #9904, .F. ) ;
#19645=ORIENTED_EDGE ( 'NONE', *, *, #24530, .F. ) ;
#19704=DIRECTION ( 'NONE',  ( 0.000000000000000000, -0.3818493186865936084, 0.9242245927363024194 ) ) ;
#19724=ORIENTED_EDGE ( 'NONE', *, *, #30077, .T. ) ;
#19731=ADVANCED_FACE ( 'NONE', ( #37408 ), #3102, .T. ) ;
#19759=EDGE_CURVE ( 'NONE', #17628, #41162, #17684, .T. ) ;
#19794=FACE_OUTER_BOUND ( 'NONE', #6697, .T. ) ;
#19803=DIRECTION ( 'NONE',  ( 1.000000000000000000, 0.000000000000000000, -0.000000000000000000 ) ) ;
#19806=CIRCLE ( 'NONE', #15438, 2.000000000000000444 ) ;
#19812=EDGE_CURVE ( 'NONE', #41036, #20548, #897, .T. ) ;
#19814=AXIS2_PLACEMENT_3D ( 'NONE', #21189, #31223, #31544 ) ;
#19830=AXIS2_PLACEMENT_3D ( 'NONE', #33912, #13196, #30736 ) ;
#19845=CARTESIAN_POINT ( 'NONE',  ( 89.40092984481313465, -25.99489077589524300, -13.39321520033831625 ) ) ;
#19848=DIRECTION ( 'NONE',  ( 1.000000000000000000, 0.000000000000000000, -0.000000000000000000 ) ) ;
#19869=ORIENTED_EDGE ( 'NONE', *, *, #13069, .F. ) ;
#19874=ORIENTED_EDGE ( 'NONE', *, *, #11421, .T. ) ;
#19880=ORIENTED_EDGE ( 'NONE', *, *, #17775, .F. ) ;
#19900=AXIS2_PLACEMENT_3D ( 'NONE', #3798, #6569, #34366 ) ;
#19905=ORIENTED_EDGE ( 'NONE', *, *, #29473, .F. ) ;
#19939=VERTEX_POINT ( 'NONE', #4989 ) ;
#19992=VERTEX_POINT ( 'NONE', #22999 ) ;
#20035=CIRCLE ( 'NONE', #20741, 1.610000000000000986 ) ;
#20048=ORIENTED_EDGE ( 'NONE', *, *, #5411, .F. ) ;
#20054=EDGE_CURVE ( 'NONE', #35629, #10759, #1649, .T. ) ;
#20066=CARTESIAN_POINT ( 'NONE',  ( 87.02785693856107230, -24.14644159042263993, -12.62951656296512937 ) ) ;
#20087=CARTESIAN_POINT ( 'NONE',  ( 89.67401078471493747, -24.14644159042263993, -12.62951656296512937 ) ) ;
#20092=ORIENTED_EDGE ( 'NONE', *, *, #11363, .F. ) ;
#20115=CIRCLE ( 'NONE', #32457, 2.000000000000000444 ) ;
#20151=CARTESIAN_POINT ( 'NONE',  ( 89.67401078471493747, -25.99489077589524300, -13.39321520033831447 ) ) ;
#20154=CONICAL_SURFACE ( 'NONE', #1890, 0.8509999999999994236, 0.06981317007976593769 ) ;
#20175=ORIENTED_EDGE ( 'NONE', *, *, #25053, .T. ) ;
#20176=PLANE ( 'NONE',  #43389 ) ;
#20184=DIRECTION ( 'NONE',  ( 0.000000000000000000, -0.9242245927363029745, -0.3818493186865927203 ) ) ;
#20190=DIRECTION ( 'NONE',  ( 0.000000000000000000, 0.3818493186865929423, -0.9242245927363028635 ) ) ;
#20212=VERTEX_POINT ( 'NONE', #38031 ) ;
#20223=DIRECTION ( 'NONE',  ( 1.000000000000000000, 0.000000000000000000, -0.000000000000000000 ) ) ;
#20237=CARTESIAN_POINT ( 'NONE',  ( 84.49707967414211396, -26.75858941326842810, -11.54476601486570964 ) ) ;
#20253=DIRECTION ( 'NONE',  ( 0.000000000000000000, -0.3818493186865927203, 0.9242245927363029745 ) ) ;
#20282=DIRECTION ( 'NONE',  ( 0.000000000000000000, -0.3818493186865927203, 0.9242245927363029745 ) ) ;
#20314=ORIENTED_EDGE ( 'NONE', *, *, #39875, .T. ) ;
#20320=CARTESIAN_POINT ( 'NONE',  ( 83.44708369096697709, -25.99489077589524300, -13.39321520033831625 ) ) ;
#20343=CIRCLE ( 'NONE', #24714, 6.426280380454326924 ) ;
#20354=ORIENTED_EDGE ( 'NONE', *, *, #30585, .T. ) ;
#20362=ORIENTED_EDGE ( 'NONE', *, *, #20396, .F. ) ;
#20376=AXIS2_PLACEMENT_3D ( 'NONE', #25415, #14473, #35875 ) ;
#20380=CIRCLE ( 'NONE', #16737, 2.000000000000000444 ) ;
#20387=CARTESIAN_POINT ( 'NONE',  ( 83.72016463086879412, -26.75858941326842810, -11.54476601486570964 ) ) ;
#20396=EDGE_CURVE ( 'NONE', #35058, #7733, #9721, .T. ) ;
#20399=ORIENTED_EDGE ( 'NONE', *, *, #37934, .F. ) ;
#20403=DIRECTION ( 'NONE',  ( 1.000000000000000000, 0.000000000000000000, -0.000000000000000000 ) ) ;
#20426=DIRECTION ( 'NONE',  ( 0.000000000000000000, -0.3818493186865927203, 0.9242245927363029745 ) ) ;
#20441=CONICAL_SURFACE ( 'NONE', #12422, 2.000000000000000444, 0.9599310885968830309 ) ;
#20514=LINE ( 'NONE', #6828, #15626 ) ;
#20526=DIRECTION ( 'NONE',  ( -0.8949343913984424415, -0.1703803081152067966, 0.4123869368673871993 ) ) ;
#20527=VECTOR ( 'NONE', #44951, 1000.000000000000000 ) ;
#20548=VERTEX_POINT ( 'NONE', #40156 ) ;
#20549=DIRECTION ( 'NONE',  ( 0.000000000000000000, -0.9242245927363027524, -0.3818493186865929978 ) ) ;
#20576=EDGE_LOOP ( 'NONE', ( #23588, #43544, #25761, #18502 ) ) ;
#20601=AXIS2_PLACEMENT_3D ( 'NONE', #9937, #17008, #23386 ) ;
#20611=AXIS2_PLACEMENT_3D ( 'NONE', #40234, #39778, #19704 ) ;
#20622=VECTOR ( 'NONE', #10720, 1000.000000000000114 ) ;
#20623=DIRECTION ( 'NONE',  ( 0.000000000000000000, -0.9242245927363029745, -0.3818493186865927758 ) ) ;
#20624=DIRECTION ( 'NONE',  ( 0.000000000000000000, 0.3818493186865927203, -0.9242245927363029745 ) ) ;
#20634=AXIS2_PLACEMENT_3D ( 'NONE', #21378, #25026, #4941 ) ;
#20647=LINE ( 'NONE', #44144, #23527 ) ;
#20674=ORIENTED_EDGE ( 'NONE', *, *, #33820, .F. ) ;
#20688=DIRECTION ( 'NONE',  ( 1.000000000000000000, 0.000000000000000000, -0.000000000000000000 ) ) ;
#20721=DIRECTION ( 'NONE',  ( 0.000000000000000000, -0.3818493186865927203, 0.9242245927363029745 ) ) ;
#20741=AXIS2_PLACEMENT_3D ( 'NONE', #7474, #36190, #38707 ) ;
#20743=ORIENTED_EDGE ( 'NONE', *, *, #15899, .T. ) ;
#20746=CARTESIAN_POINT ( 'NONE',  ( 87.02785693856107230, -25.99489077589524300, -13.39321520033831447 ) ) ;
#20766=CARTESIAN_POINT ( 'NONE',  ( 96.54708369096698561, -26.33989114581222424, -11.20947992683166916 ) ) ;
#20768=ORIENTED_EDGE ( 'NONE', *, *, #40341, .F. ) ;
#20770=DIRECTION ( 'NONE',  ( 0.000000000000000000, -0.3818493186865927203, 0.9242245927363029745 ) ) ;
#20774=CARTESIAN_POINT ( 'NONE',  ( 83.44708369096697709, -26.60966817898065884, -11.90521360603286816 ) ) ;
#20797=VECTOR ( 'NONE', #41334, 1000.000000000000114 ) ;
#20812=DIRECTION ( 'NONE',  ( -0.4461977533474358326, 0.3417300876246960328, -0.8271203734159366938 ) ) ;
#20823=VERTEX_POINT ( 'NONE', #15762 ) ;
#20827=EDGE_LOOP ( 'NONE', ( #5088, #22873, #15322, #19592, #24420 ) ) ;
#20835=CIRCLE ( 'NONE', #14289, 0.8509999999999994236 ) ;
#20837=ORIENTED_EDGE ( 'NONE', *, *, #8038, .T. ) ;
#20846=VERTEX_POINT ( 'NONE', #26244 ) ;
#20852=VECTOR ( 'NONE', #25183, 1000.000000000000000 ) ;
#20863=EDGE_CURVE ( 'NONE', #30793, #25225, #22819, .T. ) ;
#20869=DIRECTION ( 'NONE',  ( 1.000000000000000000, 0.000000000000000000, -0.000000000000000000 ) ) ;
#20879=EDGE_CURVE ( 'NONE', #1042, #17628, #41955, .T. ) ;
#20895=CARTESIAN_POINT ( 'NONE',  ( 94.20708369096698220, -26.78140590431383572, -13.71816897054060469 ) ) ;
#20904=CIRCLE ( 'NONE', #33247, 4.000000000000000888 ) ;
#20910=ORIENTED_EDGE ( 'NONE', *, *, #21656, .T. ) ;
#20913=CARTESIAN_POINT ( 'NONE',  ( 94.20708369096698220, -27.10035099198479358, -13.29271931396930739 ) ) ;
#20921=CARTESIAN_POINT ( 'NONE',  ( 87.14323352029596492, -27.84333996136784961, -14.15691383771150136 ) ) ;
#20924=CARTESIAN_POINT ( 'NONE',  ( 83.83554121260367253, -25.99489077589524300, -13.39321520033831625 ) ) ;
#20987=ORIENTED_EDGE ( 'NONE', *, *, #16294, .F. ) ;
#21041=ORIENTED_EDGE ( 'NONE', *, *, #42209, .F. ) ;
#21043=CARTESIAN_POINT ( 'NONE',  ( 96.21525317080913453, -26.27671625074736994, -11.36238786408634738 ) ) ;
#21065=CYLINDRICAL_SURFACE ( 'NONE', #31966, 4.000000000000000888 ) ;
#21109=EDGE_CURVE ( 'NONE', #13898, #21831, #36162, .T. ) ;
#21116=EDGE_CURVE ( 'NONE', #38150, #12241, #11181, .T. ) ;
#21118=CARTESIAN_POINT ( 'NONE',  ( 89.12784890491134604, -26.75858941326842810, -11.54476601486570964 ) ) ;
#21135=DIRECTION ( 'NONE',  ( 0.000000000000000000, -0.3818493186865936084, 0.9242245927363024194 ) ) ;
#21144=EDGE_CURVE ( 'NONE', #28337, #2441, #34456, .T. ) ;
#21146=DIRECTION ( 'NONE',  ( 1.000000000000000000, 0.000000000000000000, -0.000000000000000000 ) ) ;
#21159=DIRECTION ( 'NONE',  ( 0.000000000000000000, -0.3818493186865936084, 0.9242245927363024194 ) ) ;
#21176=CIRCLE ( 'NONE', #36463, 2.000000000000000444 ) ;
#21179=CARTESIAN_POINT ( 'NONE',  ( 95.28169473643895060, -25.99489077589524300, -13.39321520033831447 ) ) ;
#21189=CARTESIAN_POINT ( 'NONE',  ( 90.72400676789006013, -25.99489077589524300, -13.39321520033831625 ) ) ;
#21193=ADVANCED_FACE ( 'NONE', ( #29779 ), #12466, .T. ) ;
#21196=CARTESIAN_POINT ( 'NONE',  ( 121.9470836909669913, -25.99489077589524300, -13.39321520033831447 ) ) ;
#21207=CARTESIAN_POINT ( 'NONE',  ( 94.99177781699742695, -29.69178914684045623, -14.92061247508468647 ) ) ;
#21215=AXIS2_PLACEMENT_3D ( 'NONE', #28968, #25096, #35557 ) ;
#21228=CIRCLE ( 'NONE', #35029, 3.853420195439741125 ) ;
#21245=ORIENTED_EDGE ( 'NONE', *, *, #16414, .T. ) ;
#21251=CYLINDRICAL_SURFACE ( 'NONE', #39490, 1.999999999999998890 ) ;
#21259=ADVANCED_FACE ( 'NONE', ( #1291 ), #35203, .T. ) ;
#21265=ORIENTED_EDGE ( 'NONE', *, *, #19629, .F. ) ;
#21267=DIRECTION ( 'NONE',  ( -0.5735764363510446051, 0.3127926500124816878, -0.7570804645221042017 ) ) ;
#21286=ORIENTED_EDGE ( 'NONE', *, *, #37861, .F. ) ;
#21290=CIRCLE ( 'NONE', #22005, 2.000000000000000444 ) ;
#21297=DIRECTION ( 'NONE',  ( 0.8949343913984423304, 0.1703803081152067689, -0.4123869368673877545 ) ) ;
#21305=ORIENTED_EDGE ( 'NONE', *, *, #301, .T. ) ;
#21313=FACE_OUTER_BOUND ( 'NONE', #14658, .T. ) ;
#21347=VERTEX_POINT ( 'NONE', #2863 ) ;
#21368=CARTESIAN_POINT ( 'NONE',  ( 86.36631847702263087, -25.99489077589524300, -13.39321520033831447 ) ) ;
#21369=CONICAL_SURFACE ( 'NONE', #245, 2.000000000000000444, 0.9599310885968830309 ) ;
#21378=CARTESIAN_POINT ( 'NONE',  ( 87.68939540009954214, -25.99489077589524300, -13.39321520033831447 ) ) ;
#21381=AXIS2_PLACEMENT_3D ( 'NONE', #12755, #41035, #40570 ) ;
#21412=ORIENTED_EDGE ( 'NONE', *, *, #7719, .T. ) ;
#21419=EDGE_LOOP ( 'NONE', ( #9900, #21412, #5502, #29386, #37624 ) ) ;
#21429=CARTESIAN_POINT ( 'NONE',  ( 84.49707967414211396, -25.99489077589524300, -13.39321520033831625 ) ) ;
#21444=VERTEX_POINT ( 'NONE', #16 ) ;
#21446=CARTESIAN_POINT ( 'NONE',  ( 90.45092582798827152, -25.23119213852205789, -15.24166438581092109 ) ) ;
#21447=CARTESIAN_POINT ( 'NONE',  ( 86.75477599865929790, -25.99489077589524300, -13.39321520033831625 ) ) ;
#21461=ORIENTED_EDGE ( 'NONE', *, *, #42966, .T. ) ;
#21472=LINE ( 'NONE', #42228, #9599 ) ;
#21484=FACE_OUTER_BOUND ( 'NONE', #22395, .T. ) ;
#21492=ORIENTED_EDGE ( 'NONE', *, *, #25481, .F. ) ;
#21520=ORIENTED_EDGE ( 'NONE', *, *, #30040, .F. ) ;
#21522=CARTESIAN_POINT ( 'NONE',  ( 92.04708369096698561, -26.60966817898065884, -11.90521360603286816 ) ) ;
#21534=CIRCLE ( 'NONE', #22282, 2.000000000000000444 ) ;
#21542=VERTEX_POINT ( 'NONE', #36452 ) ;
#21554=CYLINDRICAL_SURFACE ( 'NONE', #41025, 1.999999999999998890 ) ;
#21558=EDGE_CURVE ( 'NONE', #2441, #17646, #2246, .T. ) ;
#21560=CARTESIAN_POINT ( 'NONE',  ( 88.73939138327467901, -26.60966817898065884, -11.90521360603286816 ) ) ;
#21567=AXIS2_PLACEMENT_3D ( 'NONE', #17975, #18201, #31650 ) ;
#21568=CARTESIAN_POINT ( 'NONE',  ( 87.80477198183443477, -27.84333996136784961, -14.15691383771150136 ) ) ;
#21602=AXIS2_PLACEMENT_3D ( 'NONE', #21807, #14747, #22034 ) ;
#21607=ORIENTED_EDGE ( 'NONE', *, *, #42473, .T. ) ;
#21621=DIRECTION ( 'NONE',  ( 1.000000000000000000, 0.000000000000000000, -0.000000000000000000 ) ) ;
#21637=ORIENTED_EDGE ( 'NONE', *, *, #27287, .T. ) ;
#21649=DIRECTION ( 'NONE',  ( 0.000000000000000000, 0.000000000000000000, 1.000000000000000000 ) ) ;
#21656=EDGE_CURVE ( 'NONE', #31533, #23066, #12532, .T. ) ;
#21659=CIRCLE ( 'NONE', #32581, 1.610000000000000986 ) ;
#21671=AXIS2_PLACEMENT_3D ( 'NONE', #11538, #12440, #19276 ) ;
#21675=FACE_OUTER_BOUND ( 'NONE', #1647, .T. ) ;
#21684=ADVANCED_FACE ( 'NONE', ( #36897 ), #24307, .T. ) ;
#21688=ADVANCED_FACE ( 'NONE', ( #44446 ), #40339, .T. ) ;
#21693=CARTESIAN_POINT ( 'NONE',  ( 86.36631847702263087, -25.99489077589524300, -13.39321520033831447 ) ) ;
#21703=ADVANCED_FACE ( 'NONE', ( #23238 ), #14832, .T. ) ;
#21746=EDGE_LOOP ( 'NONE', ( #26683, #35881, #28954, #31471, #3628 ) ) ;
#21752=CARTESIAN_POINT ( 'NONE',  ( 85.15861813568058380, -25.23119213852205789, -15.24166438581092109 ) ) ;
#21765=CARTESIAN_POINT ( 'NONE',  ( 121.9470836909669913, -27.84333996136784961, -14.15691383771150136 ) ) ;
#21768=EDGE_LOOP ( 'NONE', ( #33638, #42476, #42442, #10226, #9090, #7840, #29166 ) ) ;
#21772=ADVANCED_FACE ( 'NONE', ( #23004 ), #19585, .T. ) ;
#21791=DIRECTION ( 'NONE',  ( 0.000000000000000000, -0.9242245927363028635, -0.3818493186865927758 ) ) ;
#21796=VERTEX_POINT ( 'NONE', #30753 ) ;
#21807=CARTESIAN_POINT ( 'NONE',  ( 94.20708369096698220, -25.99489077589524300, -13.39321520033831447 ) ) ;
#21820=EDGE_CURVE ( 'NONE', #9155, #14958, #19195, .T. ) ;
#21831=VERTEX_POINT ( 'NONE', #3385 ) ;
#21832=CIRCLE ( 'NONE', #29122, 2.000000000000000444 ) ;
#21861=ORIENTED_EDGE ( 'NONE', *, *, #24038, .F. ) ;
#21875=DIRECTION ( 'NONE',  ( 1.000000000000000000, 0.000000000000000000, -0.000000000000000000 ) ) ;
#21877=CARTESIAN_POINT ( 'NONE',  ( 96.54708369096698561, -24.69793907545987466, -15.18364567559777178 ) ) ;
#21884=VERTEX_POINT ( 'NONE', #45115 ) ;
#21897=CARTESIAN_POINT ( 'NONE',  ( 89.01247232317646763, -25.99489077589524300, -13.39321520033831447 ) ) ;
#21908=CARTESIAN_POINT ( 'NONE',  ( 85.43169907558235820, -25.38011337280982715, -14.88121679464376257 ) ) ;
#21924=VERTEX_POINT ( 'NONE', #35031 ) ;
#21936=CARTESIAN_POINT ( 'NONE',  ( 94.86797725101187950, -25.11844467255894031, -13.58832973634262409 ) ) ;
#21941=EDGE_CURVE ( 'NONE', #39054, #34542, #23575, .T. ) ;
#21964=EDGE_LOOP ( 'NONE', ( #6571, #12288, #31025, #22609, #36979 ) ) ;
#21970=EDGE_LOOP ( 'NONE', ( #1842, #11916, #26469, #42665, #43164, #31572 ) ) ;
#21982=CIRCLE ( 'NONE', #2311, 2.000000000000000444 ) ;
#21988=CYLINDRICAL_SURFACE ( 'NONE', #37202, 1.999999999999998890 ) ;
#22002=DIRECTION ( 'NONE',  ( 0.000000000000000000, -0.9242245927363028635, -0.3818493186865930533 ) ) ;
#22005=AXIS2_PLACEMENT_3D ( 'NONE', #30950, #17278, #27987 ) ;
#22034=DIRECTION ( 'NONE',  ( 0.000000000000000000, -0.9242245927363029745, -0.3818493186865927758 ) ) ;
#22058=DIRECTION ( 'NONE',  ( 0.000000000000000000, 0.3818493186865927203, -0.9242245927363029745 ) ) ;
#22069=DIRECTION ( 'NONE',  ( 1.000000000000000000, 0.000000000000000000, -0.000000000000000000 ) ) ;
#22076=ADVANCED_FACE ( 'NONE', ( #23929 ), #17031, .T. ) ;
#22078=EDGE_CURVE ( 'NONE', #9582, #2844, #31547, .T. ) ;
#22089=AXIS2_PLACEMENT_3D ( 'NONE', #29622, #22552, #33020 ) ;
#22099=VERTEX_POINT ( 'NONE', #28904 ) ;
#22121=SPHERICAL_SURFACE ( 'NONE', #3625, 6.500000000000000000 ) ;
#22127=DIRECTION ( 'NONE',  ( 1.000000000000000000, 0.000000000000000000, -0.000000000000000000 ) ) ;
#22134=CIRCLE ( 'NONE', #31597, 2.000000000000000444 ) ;
#22135=EDGE_LOOP ( 'NONE', ( #40537, #19493, #11233, #30816, #27532 ) ) ;
#22142=ORIENTED_EDGE ( 'NONE', *, *, #39514, .T. ) ;
#22145=DIRECTION ( 'NONE',  ( 0.000000000000000000, -0.9242245927363028635, -0.3818493186865930533 ) ) ;
#22187=CONICAL_SURFACE ( 'NONE', #22901, 1.610000000000000986, 0.9599310885968765916 ) ;
#22188=DIRECTION ( 'NONE',  ( 0.000000000000000000, -0.9242245927363028635, -0.3818493186865930533 ) ) ;
#22202=VERTEX_POINT ( 'NONE', #32312 ) ;
#22209=CARTESIAN_POINT ( 'NONE',  ( 89.67401078471493747, -26.75858941326842810, -11.54476601486570964 ) ) ;
#22224=VECTOR ( 'NONE', #18746, 1000.000000000000000 ) ;
#22247=ADVANCED_FACE ( 'NONE', ( #7921 ), #21369, .T. ) ;
#22266=DIRECTION ( 'NONE',  ( -1.000000000000000000, 0.000000000000000000, 0.000000000000000000 ) ) ;
#22274=EDGE_CURVE ( 'NONE', #31284, #17364, #8256, .T. ) ;
#22277=EDGE_CURVE ( 'NONE', #35171, #36351, #11576, .T. ) ;
#22282=AXIS2_PLACEMENT_3D ( 'NONE', #37275, #29997, #36820 ) ;
#22283=DIRECTION ( 'NONE',  ( 0.000000000000000000, -0.3818493186865936084, 0.9242245927363024194 ) ) ;
#22295=CARTESIAN_POINT ( 'NONE',  ( 89.78938736644981589, -25.99489077589524300, -13.39321520033831625 ) ) ;
#22306=ORIENTED_EDGE ( 'NONE', *, *, #21116, .F. ) ;
#22310=FACE_OUTER_BOUND ( 'NONE', #41131, .T. ) ;
#22331=CONICAL_SURFACE ( 'NONE', #6317, 2.000000000000000444, 0.9599310885968830309 ) ;
#22344=DIRECTION ( 'NONE',  ( 0.000000000000000000, -0.3818493186865927203, 0.9242245927363029745 ) ) ;
#22359=ORIENTED_EDGE ( 'NONE', *, *, #5500, .F. ) ;
#22365=ORIENTED_EDGE ( 'NONE', *, *, #22503, .F. ) ;
#22377=VECTOR ( 'NONE', #24414, 1000.000000000000114 ) ;
#22383=ORIENTED_EDGE ( 'NONE', *, *, #30360, .F. ) ;
#22391=CIRCLE ( 'NONE', #4298, 2.000000000000000444 ) ;
#22394=VERTEX_POINT ( 'NONE', #25708 ) ;
#22395=EDGE_LOOP ( 'NONE', ( #31067, #12953, #7744, #41468, #27789, #41140 ) ) ;
#22403=ADVANCED_FACE ( 'NONE', ( #36175 ), #5349, .T. ) ;
#22427=CARTESIAN_POINT ( 'NONE',  ( 90.48265143217095385, -25.66130191030491758, -14.20063063452593255 ) ) ;
#22437=ORIENTED_EDGE ( 'NONE', *, *, #3000, .T. ) ;
#22441=VECTOR ( 'NONE', #25297, 1000.000000000000114 ) ;
#22456=CARTESIAN_POINT ( 'NONE',  ( 95.28169473643895060, -29.55631648666738087, -14.86464107658013845 ) ) ;
#22463=DIRECTION ( 'NONE',  ( 0.000000000000000000, -0.9242245927363041957, -0.3818493186865896671 ) ) ;
#22472=EDGE_CURVE ( 'NONE', #41351, #13898, #33720, .T. ) ;
#22501=DIRECTION ( 'NONE',  ( 0.000000000000000000, -0.3818493186865927203, 0.9242245927363029745 ) ) ;
#22503=EDGE_CURVE ( 'NONE', #28262, #24082, #12480, .T. ) ;
#22519=ADVANCED_FACE ( 'NONE', ( #40745 ), #18449, .T. ) ;
#22523=EDGE_CURVE ( 'NONE', #3446, #21884, #39838, .T. ) ;
#22535=CIRCLE ( 'NONE', #1406, 1.610000000000000986 ) ;
#22552=DIRECTION ( 'NONE',  ( -1.000000000000000000, 0.000000000000000000, 0.000000000000000000 ) ) ;
#22553=ORIENTED_EDGE ( 'NONE', *, *, #9845, .F. ) ;
#22576=EDGE_CURVE ( 'NONE', #12871, #10499, #38133, .T. ) ;
#22599=CIRCLE ( 'NONE', #43008, 2.000000000000000444 ) ;
#22604=VERTEX_POINT ( 'NONE', #5397 ) ;
#22609=ORIENTED_EDGE ( 'NONE', *, *, #11114, .F. ) ;
#22621=EDGE_LOOP ( 'NONE', ( #28348, #17385, #12413, #41797, #849 ) ) ;
#22622=DIRECTION ( 'NONE',  ( -1.000000000000000000, 0.000000000000000000, 0.000000000000000000 ) ) ;
#22635=VECTOR ( 'NONE', #10430, 999.9999999999998863 ) ;
#22636=DIRECTION ( 'NONE',  ( 1.000000000000000000, 0.000000000000000000, -0.000000000000000000 ) ) ;
#22685=CARTESIAN_POINT ( 'NONE',  ( 121.9470836909669913, -25.99489077589524300, -13.39321520033831447 ) ) ;
#22694=CARTESIAN_POINT ( 'NONE',  ( 96.54708369096698561, -27.78532125115470208, -14.69016690077367926 ) ) ;
#22732=LINE ( 'NONE', #12943, #35444 ) ;
#22740=ORIENTED_EDGE ( 'NONE', *, *, #30620, .F. ) ;
#22755=ORIENTED_EDGE ( 'NONE', *, *, #18366, .T. ) ;
#22769=CARTESIAN_POINT ( 'NONE',  ( 94.20708369096698220, -26.09538666226425363, -14.49867541642786861 ) ) ;
#22786=LINE ( 'NONE', #1803, #5585 ) ;
#22802=CARTESIAN_POINT ( 'NONE',  ( 89.67401078471493747, -25.99489077589524300, -13.39321520033831447 ) ) ;
#22812=CARTESIAN_POINT ( 'NONE',  ( 121.9470836909669913, -25.99489077589524300, -13.39321520033831447 ) ) ;
#22817=EDGE_CURVE ( 'NONE', #13419, #24082, #35212, .T. ) ;
#22819=LINE ( 'NONE', #8918, #40276 ) ;
#22823=VECTOR ( 'NONE', #32068, 1000.000000000000000 ) ;
#22827=CARTESIAN_POINT ( 'NONE',  ( 121.9470836909669913, -27.84333996136784961, -14.15691383771150136 ) ) ;
#22843=VERTEX_POINT ( 'NONE', #4896 ) ;
#22847=CARTESIAN_POINT ( 'NONE',  ( 96.54708369096698561, -27.29184247633061489, -11.60278472507885894 ) ) ;
#22848=CARTESIAN_POINT ( 'NONE',  ( 121.9470836909669913, -25.99489077589524300, -13.39321520033831447 ) ) ;
#22858=VERTEX_POINT ( 'NONE', #18813 ) ;
#22867=CARTESIAN_POINT ( 'NONE',  ( 90.06246830635160450, -25.38011337280982715, -14.88121679464376257 ) ) ;
#22873=ORIENTED_EDGE ( 'NONE', *, *, #31477, .T. ) ;
#22891=ORIENTED_EDGE ( 'NONE', *, *, #30487, .F. ) ;
#22901=AXIS2_PLACEMENT_3D ( 'NONE', #13837, #17700, #31600 ) ;
#22903=CARTESIAN_POINT ( 'NONE',  ( 93.44708369096697709, -25.23119213852205789, -15.24166438581092109 ) ) ;
#22913=CARTESIAN_POINT ( 'NONE',  ( 86.75477599865929790, -26.60966817898065884, -11.90521360603286816 ) ) ;
#22927=CARTESIAN_POINT ( 'NONE',  ( 1093.930577029472943, -25.99489077589524300, -13.39321520033831447 ) ) ;
#22939=DIRECTION ( 'NONE',  ( 0.5735764363510499342, 0.3127926500124801890, -0.7570804645221008711 ) ) ;
#22955=ORIENTED_EDGE ( 'NONE', *, *, #12048, .T. ) ;
#22958=CARTESIAN_POINT ( 'NONE',  ( 93.44708369096697709, -25.99489077589524300, -13.39321520033831447 ) ) ;
#22962=CARTESIAN_POINT ( 'NONE',  ( 83.72016463086879412, -27.84333996136784961, -14.15691383771150136 ) ) ;
#22983=DIRECTION ( 'NONE',  ( 0.000000000000000000, -0.9242245927363028635, -0.3818493186865930533 ) ) ;
#22986=CARTESIAN_POINT ( 'NONE',  ( 85.82015659721905365, -26.75858941326842810, -11.54476601486570964 ) ) ;
#22999=CARTESIAN_POINT ( 'NONE',  ( 90.33554924625337890, -26.75858941326842810, -11.54476601486570964 ) ) ;
#23004=FACE_OUTER_BOUND ( 'NONE', #30143, .T. ) ;
#23005=ORIENTED_EDGE ( 'NONE', *, *, #38423, .T. ) ;
#23015=DIRECTION ( 'NONE',  ( 0.3090169943749413450, -0.8789898214420970302, -0.3631602827797496547 ) ) ;
#23032=VERTEX_POINT ( 'NONE', #22456 ) ;
#23033=DIRECTION ( 'NONE',  ( 1.000000000000000000, 0.000000000000000000, -0.000000000000000000 ) ) ;
#23040=ORIENTED_EDGE ( 'NONE', *, *, #22472, .F. ) ;
#23045=EDGE_CURVE ( 'NONE', #28442, #10907, #29526, .T. ) ;
#23066=VERTEX_POINT ( 'NONE', #40011 ) ;
#23079=CARTESIAN_POINT ( 'NONE',  ( 85.82015659721905365, -25.99489077589524300, -13.39321520033831625 ) ) ;
#23111=EDGE_LOOP ( 'NONE', ( #32392, #7281 ) ) ;
#23165=CARTESIAN_POINT ( 'NONE',  ( 96.54708369096698561, -24.20446030063578391, -12.09626349990295147 ) ) ;
#23167=CIRCLE ( 'NONE', #23891, 2.000000000000000444 ) ;
#23206=EDGE_LOOP ( 'NONE', ( #39353, #24621, #12147, #2482, #21286 ) ) ;
#23215=DIRECTION ( 'NONE',  ( 1.000000000000000000, 0.000000000000000000, -0.000000000000000000 ) ) ;
#23238=FACE_OUTER_BOUND ( 'NONE', #14373, .T. ) ;
#23239=ORIENTED_EDGE ( 'NONE', *, *, #10985, .F. ) ;
#23247=CARTESIAN_POINT ( 'NONE',  ( 121.9470836909669913, -27.84333996136784961, -14.15691383771150136 ) ) ;
#23297=EDGE_LOOP ( 'NONE', ( #44656, #19905, #16458, #246, #3652 ) ) ;
#23304=DIRECTION ( 'NONE',  ( 0.000000000000000000, -0.9242245927363028635, -0.3818493186865930533 ) ) ;
#23315=DIRECTION ( 'NONE',  ( -0.5735764363510446051, 0.3127926500124816878, -0.7570804645221042017 ) ) ;
#23331=CARTESIAN_POINT ( 'NONE',  ( 90.72400676789006013, -26.60966817898065884, -11.90521360603286816 ) ) ;
#23334=DIRECTION ( 'NONE',  ( 1.000000000000000000, 0.000000000000000000, -0.000000000000000000 ) ) ;
#23335=CARTESIAN_POINT ( 'NONE',  ( 94.20708369096698220, -25.89439488952623591, -12.28775498424876211 ) ) ;
#23358=EDGE_CURVE ( 'NONE', #36439, #31222, #27958, .T. ) ;
#23360=FACE_OUTER_BOUND ( 'NONE', #18327, .T. ) ;
#23380=ORIENTED_EDGE ( 'NONE', *, *, #11652, .F. ) ;
#23386=DIRECTION ( 'NONE',  ( 0.000000000000000000, -0.3818493186865927203, 0.9242245927363029745 ) ) ;
#23422=DIRECTION ( 'NONE',  ( 0.000000000000000000, -0.3818493186865927203, 0.9242245927363029745 ) ) ;
#23439=DIRECTION ( 'NONE',  ( 0.000000000000000000, -0.3818493186865927203, 0.9242245927363029745 ) ) ;
#23448=CARTESIAN_POINT ( 'NONE',  ( 87.80477198183443477, -25.99489077589524300, -13.39321520033831625 ) ) ;
#23457=ORIENTED_EDGE ( 'NONE', *, *, #19492, .T. ) ;
#23527=VECTOR ( 'NONE', #40949, 1000.000000000000114 ) ;
#23538=EDGE_LOOP ( 'NONE', ( #22891, #4813, #6861, #44345, #23380 ) ) ;
#23545=DIRECTION ( 'NONE',  ( 0.000000000000000000, -0.9242245927363028635, -0.3818493186865930533 ) ) ;
#23559=AXIS2_PLACEMENT_3D ( 'NONE', #10979, #18267, #38776 ) ;
#23574=VERTEX_POINT ( 'NONE', #26058 ) ;
#23575=CIRCLE ( 'NONE', #1695, 2.000000000000000444 ) ;
#23576=CARTESIAN_POINT ( 'NONE',  ( 92.04708369096698561, -26.60966817898065884, -11.90521360603286816 ) ) ;
#23588=ORIENTED_EDGE ( 'NONE', *, *, #35361, .T. ) ;
#23590=CIRCLE ( 'NONE', #35094, 2.000000000000000444 ) ;
#23610=CARTESIAN_POINT ( 'NONE',  ( 96.46827370896536991, -26.60028948451273223, -14.20056342530837412 ) ) ;
#23611=CARTESIAN_POINT ( 'NONE',  ( 87.02785693856107230, -25.99489077589524300, -13.39321520033831447 ) ) ;
#23639=ORIENTED_EDGE ( 'NONE', *, *, #37070, .F. ) ;
#23642=MECHANICAL_DESIGN_GEOMETRIC_PRESENTATION_REPRESENTATION('',(#13452),#29447);
#23675=VECTOR ( 'NONE', #41045, 1000.000000000000000 ) ;
#23678=FACE_OUTER_BOUND ( 'NONE', #20827, .T. ) ;
#23715=AXIS2_PLACEMENT_3D ( 'NONE', #16537, #37948, #20184 ) ;
#23730=LINE ( 'NONE', #30781, #15905 ) ;
#23768=CARTESIAN_POINT ( 'NONE',  ( 87.14323352029596492, -24.14644159042263993, -12.62951656296512937 ) ) ;
#23769=DIRECTION ( 'NONE',  ( 1.000000000000000000, 0.000000000000000000, -0.000000000000000000 ) ) ;
#23817=LINE ( 'NONE', #35149, #35326 ) ;
#23818=ORIENTED_EDGE ( 'NONE', *, *, #15561, .T. ) ;
#23828=CARTESIAN_POINT ( 'NONE',  ( 89.78938736644981589, -26.75858941326842810, -11.54476601486570964 ) ) ;
#23836=FACE_OUTER_BOUND ( 'NONE', #29280, .T. ) ;
#23842=FACE_OUTER_BOUND ( 'NONE', #44215, .T. ) ;
#23854=CARTESIAN_POINT ( 'NONE',  ( 85.82015659721905365, -25.99489077589524300, -13.39321520033831625 ) ) ;
#23870=CIRCLE ( 'NONE', #19479, 1.610000000000000986 ) ;
#23879=TOROIDAL_SURFACE ( 'NONE', #21671, 2.200000000000000178, 0.2000000000000000111 ) ;
#23882=DIRECTION ( 'NONE',  ( 1.000000000000000000, 0.000000000000000000, -0.000000000000000000 ) ) ;
#23891=AXIS2_PLACEMENT_3D ( 'NONE', #17051, #34568, #37778 ) ;
#23929=FACE_OUTER_BOUND ( 'NONE', #37670, .T. ) ;
#23971=CARTESIAN_POINT ( 'NONE',  ( 87.02785693856107230, -26.75858941326842810, -11.54476601486570964 ) ) ;
#23981=ADVANCED_FACE ( 'NONE', ( #12033 ), #36400, .T. ) ;
#23990=AXIS2_PLACEMENT_3D ( 'NONE', #317, #6270, #20190 ) ;
#23996=CARTESIAN_POINT ( 'NONE',  ( 94.20708369096698220, -26.81768470319947184, -13.17593392366846672 ) ) ;
#24011=ORIENTED_EDGE ( 'NONE', *, *, #13042, .F. ) ;
#24021=EDGE_LOOP ( 'NONE', ( #4651, #32161, #15972, #21492, #27775 ) ) ;
#24034=DIRECTION ( 'NONE',  ( 0.000000000000000000, -0.9242245927363028635, -0.3818493186865930533 ) ) ;
#24038=EDGE_CURVE ( 'NONE', #36181, #24368, #21832, .T. ) ;
#24042=DIRECTION ( 'NONE',  ( 1.000000000000000000, 0.000000000000000000, -0.000000000000000000 ) ) ;
#24082=VERTEX_POINT ( 'NONE', #29802 ) ;
#24088=ORIENTED_EDGE ( 'NONE', *, *, #30782, .F. ) ;
#24100=DIRECTION ( 'NONE',  ( 0.000000000000000000, -0.3818493186865927203, 0.9242245927363029745 ) ) ;
#24110=DIRECTION ( 'NONE',  ( -0.5735764363510450492, -0.3127926500124816878, 0.7570804645221038687 ) ) ;
#24115=CARTESIAN_POINT ( 'NONE',  ( 88.46631044337289040, -25.99489077589524300, -13.39321520033831625 ) ) ;
#24124=DIRECTION ( 'NONE',  ( 0.000000000000000000, -0.3818493186865936084, 0.9242245927363024194 ) ) ;
#24127=AXIS2_PLACEMENT_3D ( 'NONE', #17582, #13273, #31036 ) ;
#24143=AXIS2_PLACEMENT_3D ( 'NONE', #22903, #15394, #19485 ) ;
#24155=DIRECTION ( 'NONE',  ( 1.000000000000000000, 0.000000000000000000, -0.000000000000000000 ) ) ;
#24157=CARTESIAN_POINT ( 'NONE',  ( 89.12784890491134604, -25.23119213852205789, -15.24166438581092109 ) ) ;
#24161=DIRECTION ( 'NONE',  ( -0.000000000000000000, -0.3818493186865896671, 0.9242245927363040847 ) ) ;
#24170=DIRECTION ( 'NONE',  ( 0.5735764363510499342, 0.3127926500124801890, -0.7570804645221008711 ) ) ;
#24187=DIRECTION ( 'NONE',  ( 1.000000000000000000, 0.000000000000000000, -0.000000000000000000 ) ) ;
#24193=EDGE_CURVE ( 'NONE', #17457, #42907, #27680, .T. ) ;
#24198=ORIENTED_EDGE ( 'NONE', *, *, #6922, .F. ) ;
#24220=VERTEX_POINT ( 'NONE', #15902 ) ;
#24250=VERTEX_POINT ( 'NONE', #358 ) ;
#24252=EDGE_CURVE ( 'NONE', #13605, #29406, #6540, .T. ) ;
#24256=LINE ( 'NONE', #16971, #9116 ) ;
#24282=LINE ( 'NONE', #10151, #38530 ) ;
#24307=CONICAL_SURFACE ( 'NONE', #41072, 1.610000000000000986, 0.9599310885968765916 ) ;
#24355=EDGE_CURVE ( 'NONE', #12871, #4353, #17465, .T. ) ;
#24360=AXIS2_PLACEMENT_3D ( 'NONE', #918, #25098, #32595 ) ;
#24368=VERTEX_POINT ( 'NONE', #38207 ) ;
#24388=DIRECTION ( 'NONE',  ( 1.000000000000000000, 0.000000000000000000, -0.000000000000000000 ) ) ;
#24400=VERTEX_POINT ( 'NONE', #14048 ) ;
#24409=ORIENTED_EDGE ( 'NONE', *, *, #15292, .F. ) ;
#24414=DIRECTION ( 'NONE',  ( 0.5735764363510498232, -0.3127926500124802445, 0.7570804645221007600 ) ) ;
#24417=VECTOR ( 'NONE', #34726, 1000.000000000000114 ) ;
#24420=ORIENTED_EDGE ( 'NONE', *, *, #27017, .F. ) ;
#24446=DIRECTION ( 'NONE',  ( 0.000000000000000000, -0.3818493186865927203, 0.9242245927363029745 ) ) ;
#24451=DIRECTION ( 'NONE',  ( 0.000000000000000000, 0.9242245927363027524, 0.3818493186865928868 ) ) ;
#24468=EDGE_LOOP ( 'NONE', ( #28737, #683, #42532, #25712 ) ) ;
#24470=EDGE_CURVE ( 'NONE', #13199, #39770, #40095, .T. ) ;
#24473=EDGE_LOOP ( 'NONE', ( #5795, #373, #35286, #10580 ) ) ;
#24477=CONICAL_SURFACE ( 'NONE', #5557, 2.000000000000000444, 0.9599310885968830309 ) ;
#24497=DIRECTION ( 'NONE',  ( 1.000000000000000000, 0.000000000000000000, -0.000000000000000000 ) ) ;
#24507=DIRECTION ( 'NONE',  ( 1.000000000000000000, 0.000000000000000000, -0.000000000000000000 ) ) ;
#24530=EDGE_CURVE ( 'NONE', #41036, #30859, #2950, .T. ) ;
#24545=CONICAL_SURFACE ( 'NONE', #7815, 1.610000000000000986, 0.9599310885968765916 ) ;
#24589=ORIENTED_EDGE ( 'NONE', *, *, #5785, .T. ) ;
#24593=DIRECTION ( 'NONE',  ( 0.000000000000000000, -0.3818493186865936084, 0.9242245927363024194 ) ) ;
#24597=CARTESIAN_POINT ( 'NONE',  ( 85.04324155394569118, -25.99489077589524300, -13.39321520033831447 ) ) ;
#24618=CARTESIAN_POINT ( 'NONE',  ( 89.40092984481313465, -26.60966817898065884, -11.90521360603286816 ) ) ;
#24621=ORIENTED_EDGE ( 'NONE', *, *, #10263, .T. ) ;
#24631=LINE ( 'NONE', #35313, #14264 ) ;
#24673=ORIENTED_EDGE ( 'NONE', *, *, #29792, .T. ) ;
#24688=DIRECTION ( 'NONE',  ( 0.000000000000000000, 0.9242245927363041957, 0.3818493186865896116 ) ) ;
#24714=AXIS2_PLACEMENT_3D ( 'NONE', #7842, #28821, #21297 ) ;
#24723=VERTEX_POINT ( 'NONE', #31480 ) ;
#24746=AXIS2_PLACEMENT_3D ( 'NONE', #32836, #39475, #8465 ) ;
#24752=AXIS2_PLACEMENT_3D ( 'NONE', #37792, #27769, #10000 ) ;
#24774=DIRECTION ( 'NONE',  ( 0.000000000000000000, -0.9242245927363028635, -0.3818493186865930533 ) ) ;
#24779=AXIS2_PLACEMENT_3D ( 'NONE', #23448, #33444, #2908 ) ;
#24792=VECTOR ( 'NONE', #3145, 999.9999999999998863 ) ;
#24811=CARTESIAN_POINT ( 'NONE',  ( 88.35093386163799778, -26.75858941326842810, -11.54476601486570964 ) ) ;
#24831=DIRECTION ( 'NONE',  ( 0.000000000000000000, -0.3818493186865927203, 0.9242245927363029745 ) ) ;
#24834=CARTESIAN_POINT ( 'NONE',  ( 84.10862215250544693, -26.60966817898065884, -11.90521360603286816 ) ) ;
#24841=DIRECTION ( 'NONE',  ( 0.000000000000000000, -0.9242245927363028635, -0.3818493186865930533 ) ) ;
#24859=ORIENTED_EDGE ( 'NONE', *, *, #6178, .F. ) ;
#24868=LINE ( 'NONE', #21446, #31391 ) ;
#24874=CARTESIAN_POINT ( 'NONE',  ( 90.45092582798827152, -25.99489077589524300, -13.39321520033831625 ) ) ;
#24881=ORIENTED_EDGE ( 'NONE', *, *, #33364, .F. ) ;
#24885=AXIS2_PLACEMENT_3D ( 'NONE', #30618, #2336, #34252 ) ;
#24894=LINE ( 'NONE', #42677, #12359 ) ;
#24923=LINE ( 'NONE', #14890, #11260 ) ;
#24937=VECTOR ( 'NONE', #39466, 1000.000000000000000 ) ;
#24948=LINE ( 'NONE', #21752, #12617 ) ;
#24971=AXIS2_PLACEMENT_3D ( 'NONE', #36223, #12073, #25976 ) ;
#25001=CARTESIAN_POINT ( 'NONE',  ( 94.86797725101196477, -26.19000531189954728, -14.26966130367462426 ) ) ;
#25026=DIRECTION ( 'NONE',  ( 1.000000000000000000, 0.000000000000000000, -0.000000000000000000 ) ) ;
#25048=ADVANCED_FACE ( 'NONE', ( #21675 ), #6604, .T. ) ;
#25053=EDGE_CURVE ( 'NONE', #39963, #21924, #10966, .T. ) ;
#25064=LINE ( 'NONE', #31006, #9626 ) ;
#25096=DIRECTION ( 'NONE',  ( 1.000000000000000000, 0.000000000000000000, -0.000000000000000000 ) ) ;
#25098=DIRECTION ( 'NONE',  ( 1.000000000000000000, 0.000000000000000000, -0.000000000000000000 ) ) ;
#25108=DIRECTION ( 'NONE',  ( 1.000000000000000000, 0.000000000000000000, -0.000000000000000000 ) ) ;
#25112=VERTEX_POINT ( 'NONE', #39224 ) ;
#25132=VERTEX_POINT ( 'NONE', #18708 ) ;
#25138=UNCERTAINTY_MEASURE_WITH_UNIT (LENGTH_MEASURE( 1.000000000000000082E-05 ), #7965, 'distance_accuracy_value', 'NONE');
#25173=ORIENTED_EDGE ( 'NONE', *, *, #9249, .T. ) ;
#25175=CARTESIAN_POINT ( 'NONE',  ( 121.9470836909669913, -27.84333996136784961, -14.15691383771150136 ) ) ;
#25182=ORIENTED_EDGE ( 'NONE', *, *, #31462, .F. ) ;
#25183=DIRECTION ( 'NONE',  ( 1.000000000000000000, 0.000000000000000000, -0.000000000000000000 ) ) ;
#25190=DIRECTION ( 'NONE',  ( 0.000000000000000000, 0.9242245927363040847, 0.3818493186865897226 ) ) ;
#25203=VECTOR ( 'NONE', #978, 1000.000000000000114 ) ;
#25225=VERTEX_POINT ( 'NONE', #11869 ) ;
#25261=AXIS2_PLACEMENT_3D ( 'NONE', #6593, #37367, #33941 ) ;
#25275=CONICAL_SURFACE ( 'NONE', #37644, 0.8509999999999994236, 0.06981317007976593769 ) ;
#25297=DIRECTION ( 'NONE',  ( -0.5735764363510450492, -0.3127926500124816878, 0.7570804645221038687 ) ) ;
#25305=DIRECTION ( 'NONE',  ( 0.000000000000000000, -0.3818493186865936084, 0.9242245927363024194 ) ) ;
#25326=DIRECTION ( 'NONE',  ( 1.000000000000000000, 0.000000000000000000, -0.000000000000000000 ) ) ;
#25341=DIRECTION ( 'NONE',  ( 1.000000000000000000, 0.000000000000000000, -0.000000000000000000 ) ) ;
#25353=CARTESIAN_POINT ( 'NONE',  ( 121.9470836909669913, -25.99489077589524300, -13.39321520033831447 ) ) ;
#25355=ADVANCED_FACE ( 'NONE', ( #26000 ), #18926, .T. ) ;
#25358=ORIENTED_EDGE ( 'NONE', *, *, #40533, .F. ) ;
#25368=CARTESIAN_POINT ( 'NONE',  ( 94.20708369096698220, -25.17209684859101415, -13.61049647700816401 ) ) ;
#25382=EDGE_CURVE ( 'NONE', #21884, #17628, #21176, .T. ) ;
#25384=LINE ( 'NONE', #28802, #14049 ) ;
#25395=FACE_OUTER_BOUND ( 'NONE', #9128, .T. ) ;
#25415=CARTESIAN_POINT ( 'NONE',  ( 121.9470836909669913, -25.99489077589524300, -13.39321520033831447 ) ) ;
#25420=EDGE_CURVE ( 'NONE', #35973, #3780, #795, .T. ) ;
#25426=ORIENTED_EDGE ( 'NONE', *, *, #13998, .T. ) ;
#25438=AXIS2_PLACEMENT_3D ( 'NONE', #18325, #543, #42725 ) ;
#25481=EDGE_CURVE ( 'NONE', #4318, #15657, #34978, .T. ) ;
#25486=AXIS2_PLACEMENT_3D ( 'NONE', #34337, #38426, #13610 ) ;
#25522=VERTEX_POINT ( 'NONE', #29637 ) ;
#25532=EDGE_LOOP ( 'NONE', ( #19869, #15055, #4235, #33781, #16747, #9670 ) ) ;
#25540=FACE_OUTER_BOUND ( 'NONE', #6130, .T. ) ;
#25556=DIRECTION ( 'NONE',  ( 0.000000000000000000, -0.3818493186865936084, 0.9242245927363024194 ) ) ;
#25569=CARTESIAN_POINT ( 'NONE',  ( 84.49707967414211396, -25.23119213852205789, -15.24166438581092109 ) ) ;
#25591=ORIENTED_EDGE ( 'NONE', *, *, #32524, .T. ) ;
#25592=CARTESIAN_POINT ( 'NONE',  ( 91.38554522942851577, -26.60966817898065884, -11.90521360603286816 ) ) ;
#25599=CIRCLE ( 'NONE', #15403, 2.000000000000000444 ) ;
#25606=DIRECTION ( 'NONE',  ( 0.000000000000000000, 0.3818493186865927203, -0.9242245927363029745 ) ) ;
#25610=CIRCLE ( 'NONE', #24885, 6.479565957685750277 ) ;
#25632=DIRECTION ( 'NONE',  ( 1.000000000000000000, 0.000000000000000000, -0.000000000000000000 ) ) ;
#25637=AXIS2_PLACEMENT_3D ( 'NONE', #7293, #17568, #20549 ) ;
#25643=FACE_OUTER_BOUND ( 'NONE', #35550, .T. ) ;
#25660=CARTESIAN_POINT ( 'NONE',  ( 121.9470836909669913, -24.14644159042263993, -12.62951656296512937 ) ) ;
#25697=CARTESIAN_POINT ( 'NONE',  ( 89.40092984481313465, -25.99489077589524300, -13.39321520033831625 ) ) ;
#25708=CARTESIAN_POINT ( 'NONE',  ( 85.15861813568058380, -26.75858941326842810, -11.54476601486570964 ) ) ;
#25709=VERTEX_POINT ( 'NONE', #30955 ) ;
#25712=ORIENTED_EDGE ( 'NONE', *, *, #19812, .F. ) ;
#25735=DIRECTION ( 'NONE',  ( 0.000000000000000000, 0.3818493186865927203, -0.9242245927363029745 ) ) ;
#25755=ORIENTED_EDGE ( 'NONE', *, *, #42112, .F. ) ;
#25761=ORIENTED_EDGE ( 'NONE', *, *, #39681, .T. ) ;
#25808=DIRECTION ( 'NONE',  ( 1.000000000000000000, 0.000000000000000000, -0.000000000000000000 ) ) ;
#25815=ORIENTED_EDGE ( 'NONE', *, *, #12499, .T. ) ;
#25819=( LENGTH_UNIT ( ) NAMED_UNIT ( * ) SI_UNIT ( .MILLI., .METRE. ) );
#25830=ORIENTED_EDGE ( 'NONE', *, *, #45086, .F. ) ;
#25847=EDGE_CURVE ( 'NONE', #31533, #8410, #42312, .T. ) ;
#25869=VECTOR ( 'NONE', #7878, 1000.000000000000114 ) ;
#25880=DIRECTION ( 'NONE',  ( 0.000000000000000000, -0.9242245927363029745, -0.3818493186865927758 ) ) ;
#25906=DIRECTION ( 'NONE',  ( 1.000000000000000000, 0.000000000000000000, -0.000000000000000000 ) ) ;
#25907=FACE_OUTER_BOUND ( 'NONE', #24468, .T. ) ;
#25916=CARTESIAN_POINT ( 'NONE',  ( 121.9470836909669913, -24.14644159042263993, -12.62951656296512937 ) ) ;
#25933=DIRECTION ( 'NONE',  ( 0.000000000000000000, -0.3818493186865927203, 0.9242245927363029745 ) ) ;
#25944=VECTOR ( 'NONE', #39510, 1000.000000000000114 ) ;
#25970=ORIENTED_EDGE ( 'NONE', *, *, #42209, .T. ) ;
#25976=DIRECTION ( 'NONE',  ( 0.000000000000000000, 0.9242245927363028635, 0.3818493186865930533 ) ) ;
#25996=DIRECTION ( 'NONE',  ( 0.000000000000000000, 0.3818493186865928868, -0.9242245927363028635 ) ) ;
#26000=FACE_OUTER_BOUND ( 'NONE', #31020, .T. ) ;
#26018=CARTESIAN_POINT ( 'NONE',  ( 91.65862616933031859, -26.75858941326842810, -11.54476601486570964 ) ) ;
#26024=ORIENTED_EDGE ( 'NONE', *, *, #25382, .F. ) ;
#26028=CONICAL_SURFACE ( 'NONE', #43481, 2.000000000000000444, 0.9599310885968830309 ) ;
#26040=CIRCLE ( 'NONE', #34045, 3.853420195439741125 ) ;
#26058=CARTESIAN_POINT ( 'NONE',  ( 89.78938736644981589, -27.84333996136784961, -14.15691383771150136 ) ) ;
#26100=FACE_OUTER_BOUND ( 'NONE', #23111, .T. ) ;
#26110=ADVANCED_FACE ( 'NONE', ( #25907 ), #19293, .T. ) ;
#26131=DIRECTION ( 'NONE',  ( 1.000000000000000000, 0.000000000000000000, -0.000000000000000000 ) ) ;
#26153=CARTESIAN_POINT ( 'NONE',  ( 94.20708369096698220, -25.14343533174585943, -14.10537061818067883 ) ) ;
#26161=CYLINDRICAL_SURFACE ( 'NONE', #41324, 1.999999999999998890 ) ;
#26172=ORIENTED_EDGE ( 'NONE', *, *, #7485, .T. ) ;
#26181=DIRECTION ( 'NONE',  ( 0.000000000000000000, -0.3818493186865936084, 0.9242245927363024194 ) ) ;
#26214=CARTESIAN_POINT ( 'NONE',  ( 88.46631044337289040, -25.99489077589524300, -13.39321520033831625 ) ) ;
#26222=AXIS2_PLACEMENT_3D ( 'NONE', #21897, #42654, #10970 ) ;
#26244=CARTESIAN_POINT ( 'NONE',  ( 84.49707967414211396, -24.14644159042263993, -12.62951656296512937 ) ) ;
#26284=VERTEX_POINT ( 'NONE', #29160 ) ;
#26301=ORIENTED_EDGE ( 'NONE', *, *, #8889, .T. ) ;
#26313=ORIENTED_EDGE ( 'NONE', *, *, #15439, .T. ) ;
#26319=ORIENTED_EDGE ( 'NONE', *, *, #17516, .F. ) ;
#26327=DIRECTION ( 'NONE',  ( 0.000000000000000000, -0.3818493186865936084, 0.9242245927363024194 ) ) ;
#26357=FACE_OUTER_BOUND ( 'NONE', #8652, .T. ) ;
#26364=DIRECTION ( 'NONE',  ( 1.000000000000000000, 0.000000000000000000, -0.000000000000000000 ) ) ;
#26367=ORIENTED_EDGE ( 'NONE', *, *, #18048, .F. ) ;
#26384=CONICAL_SURFACE ( 'NONE', #40987, 0.8509999999999994236, 0.06981317007976593769 ) ;
#26391=CARTESIAN_POINT ( 'NONE',  ( 92.32016463086877422, -26.75858941326842810, -11.54476601486570964 ) ) ;
#26439=DIRECTION ( 'NONE',  ( 0.000000000000000000, -0.3818493186865927203, 0.9242245927363029745 ) ) ;
#26442=AXIS2_PLACEMENT_3D ( 'NONE', #3961, #25632, #31780 ) ;
#26453=VECTOR ( 'NONE', #43709, 1000.000000000000114 ) ;
#26467=DIRECTION ( 'NONE',  ( 0.000000000000000000, 0.9242245927363028635, 0.3818493186865930533 ) ) ;
#26469=ORIENTED_EDGE ( 'NONE', *, *, #27126, .T. ) ;
#26480=CARTESIAN_POINT ( 'NONE',  ( 89.12784890491134604, -24.14644159042263993, -12.62951656296512937 ) ) ;
#26482=TOROIDAL_SURFACE ( 'NONE', #952, 3.640000000000000124, 0.3600000000000000422 ) ;
#26522=VERTEX_POINT ( 'NONE', #28712 ) ;
#26530=EDGE_LOOP ( 'NONE', ( #4093, #2834, #8657, #12015, #28563 ) ) ;
#26532=DIRECTION ( 'NONE',  ( 1.000000000000000000, 0.000000000000000000, -0.000000000000000000 ) ) ;
#26546=ORIENTED_EDGE ( 'NONE', *, *, #30620, .T. ) ;
#26553=FACE_OUTER_BOUND ( 'NONE', #11274, .T. ) ;
#26565=CIRCLE ( 'NONE', #39678, 2.000000000000000444 ) ;
#26572=ORIENTED_EDGE ( 'NONE', *, *, #3062, .T. ) ;
#26573=FACE_OUTER_BOUND ( 'NONE', #30758, .T. ) ;
#26599=EDGE_LOOP ( 'NONE', ( #27903, #22142, #6751, #5105, #39509 ) ) ;
#26605=DIRECTION ( 'NONE',  ( 0.000000000000000000, -0.3818493186865927203, 0.9242245927363029745 ) ) ;
#26613=DIRECTION ( 'NONE',  ( 0.000000000000000000, -0.9242245927363028635, -0.3818493186865930533 ) ) ;
#26643=ORIENTED_EDGE ( 'NONE', *, *, #40899, .F. ) ;
#26646=ORIENTED_EDGE ( 'NONE', *, *, #11421, .F. ) ;
#26665=AXIS2_PLACEMENT_3D ( 'NONE', #15488, #5215, #15259 ) ;
#26683=ORIENTED_EDGE ( 'NONE', *, *, #25847, .T. ) ;
#26687=AXIS2_PLACEMENT_3D ( 'NONE', #13892, #10254, #24161 ) ;
#26693=CARTESIAN_POINT ( 'NONE',  ( 87.68939540009954214, -27.84333996136784961, -14.15691383771150136 ) ) ;
#26711=ORIENTED_EDGE ( 'NONE', *, *, #41864, .T. ) ;
#26795=DIRECTION ( 'NONE',  ( 0.000000000000000000, -0.3818493186865936084, 0.9242245927363024194 ) ) ;
#26832=DIRECTION ( 'NONE',  ( 0.000000000000000000, -0.3818493186865927203, 0.9242245927363029745 ) ) ;
#26839=AXIS2_PLACEMENT_3D ( 'NONE', #2011, #29384, #16163 ) ;
#26841=CARTESIAN_POINT ( 'NONE',  ( 96.46827370896536991, -25.38949206727775731, -12.58586697536825660 ) ) ;
#26849=ORIENTED_EDGE ( 'NONE', *, *, #27017, .T. ) ;
#26861=DIRECTION ( 'NONE',  ( 1.000000000000000000, 0.000000000000000000, -0.000000000000000000 ) ) ;
#26897=CONICAL_SURFACE ( 'NONE', #34153, 1.610000000000000986, 0.9599310885968765916 ) ;
#26902=VECTOR ( 'NONE', #4184, 1000.000000000000114 ) ;
#26910=DIRECTION ( 'NONE',  ( 0.000000000000000000, -0.3818493186865936084, 0.9242245927363024194 ) ) ;
#26928=CARTESIAN_POINT ( 'NONE',  ( 94.99177781699742695, -29.35906829345538682, -14.78314672035751443 ) ) ;
#26933=AXIS2_PLACEMENT_3D ( 'NONE', #35664, #8091, #39095 ) ;
#26936=VERTEX_POINT ( 'NONE', #32140 ) ;
#26941=VERTEX_POINT ( 'NONE', #42422 ) ;
#26965=AXIS2_PLACEMENT_3D ( 'NONE', #28756, #18934, #25556 ) ;
#26968=ORIENTED_EDGE ( 'NONE', *, *, #18240, .F. ) ;
#26980=DIRECTION ( 'NONE',  ( 0.000000000000000000, -0.3818493186865927203, 0.9242245927363029745 ) ) ;
#27017=EDGE_CURVE ( 'NONE', #22843, #42191, #7989, .T. ) ;
#27030=CARTESIAN_POINT ( 'NONE',  ( 84.49707967414211396, -25.23119213852205789, -15.24166438581092109 ) ) ;
#27047=ORIENTED_EDGE ( 'NONE', *, *, #790, .T. ) ;
#27050=CONICAL_SURFACE ( 'NONE', #9563, 2.000000000000000444, 0.9599310885968830309 ) ;
#27054=ORIENTED_EDGE ( 'NONE', *, *, #22576, .F. ) ;
#27059=CARTESIAN_POINT ( 'NONE',  ( 94.20708369096698220, -25.99489077589524300, -13.39321520033831447 ) ) ;
#27069=DIRECTION ( 'NONE',  ( 1.000000000000000000, 0.000000000000000000, -0.000000000000000000 ) ) ;
#27071=CARTESIAN_POINT ( 'NONE',  ( 121.9470836909669913, -25.99489077589524300, -13.39321520033831447 ) ) ;
#27096=DIRECTION ( 'NONE',  ( 0.000000000000000000, -0.3818493186865927203, 0.9242245927363029745 ) ) ;
#27114=ADVANCED_FACE ( 'NONE', ( #15275 ), #22121, .T. ) ;
#27115=DIRECTION ( 'NONE',  ( 1.000000000000000000, 0.000000000000000000, -0.000000000000000000 ) ) ;
#27117=EDGE_LOOP ( 'NONE', ( #6299, #33663, #3424, #17849 ) ) ;
#27119=DIRECTION ( 'NONE',  ( 1.000000000000000000, 0.000000000000000000, -0.000000000000000000 ) ) ;
#27121=LINE ( 'NONE', #33944, #23675 ) ;
#27126=EDGE_CURVE ( 'NONE', #13419, #31913, #18251, .T. ) ;
#27169=ORIENTED_EDGE ( 'NONE', *, *, #17038, .T. ) ;
#27177=ORIENTED_EDGE ( 'NONE', *, *, #35587, .T. ) ;
#27191=ORIENTED_EDGE ( 'NONE', *, *, #23045, .F. ) ;
#27197=CIRCLE ( 'NONE', #30087, 2.000000000000000444 ) ;
#27258=CARTESIAN_POINT ( 'NONE',  ( 85.15861813568058380, -27.84333996136784961, -14.15691383771150136 ) ) ;
#27277=ORIENTED_EDGE ( 'NONE', *, *, #10583, .F. ) ;
#27287=EDGE_CURVE ( 'NONE', #19939, #5495, #24868, .T. ) ;
#27293=ORIENTED_EDGE ( 'NONE', *, *, #11769, .F. ) ;
#27317=CIRCLE ( 'NONE', #39706, 6.479565957685751165 ) ;
#27321=DIRECTION ( 'NONE',  ( -0.5735764363510450492, -0.3127926500124816878, 0.7570804645221038687 ) ) ;
#27338=EDGE_CURVE ( 'NONE', #39489, #24400, #9462, .T. ) ;
#27344=EDGE_CURVE ( 'NONE', #19363, #25522, #33456, .T. ) ;
#27378=DIRECTION ( 'NONE',  ( 0.000000000000000000, 0.3818493186865898892, -0.9242245927363040847 ) ) ;
#27386=CARTESIAN_POINT ( 'NONE',  ( 94.20708369096698220, -25.89439488952623591, -12.28775498424876211 ) ) ;
#27390=AXIS2_PLACEMENT_3D ( 'NONE', #17912, #357, #39335 ) ;
#27391=CARTESIAN_POINT ( 'NONE',  ( 83.83554121260367253, -25.99489077589524300, -13.39321520033831625 ) ) ;
#27393=CIRCLE ( 'NONE', #26665, 2.000000000000000444 ) ;
#27411=VECTOR ( 'NONE', #7421, 1000.000000000000114 ) ;
#27413=CARTESIAN_POINT ( 'NONE',  ( 85.43169907558235820, -26.60966817898065884, -11.90521360603286816 ) ) ;
#27439=ORIENTED_EDGE ( 'NONE', *, *, #44274, .F. ) ;
#27440=DIRECTION ( 'NONE',  ( 0.000000000000000000, -0.3818493186865927203, 0.9242245927363029745 ) ) ;
#27456=VECTOR ( 'NONE', #24155, 1000.000000000000000 ) ;
#27461=FACE_OUTER_BOUND ( 'NONE', #28803, .T. ) ;
#27496=CARTESIAN_POINT ( 'NONE',  ( 94.20708369096698220, -26.81768470319947184, -13.17593392366846672 ) ) ;
#27506=AXIS2_PLACEMENT_3D ( 'NONE', #38381, #17651, #14229 ) ;
#27515=AXIS2_PLACEMENT_3D ( 'NONE', #35910, #42991, #29306 ) ;
#27518=CARTESIAN_POINT ( 'NONE',  ( 84.77016061404391678, -25.99489077589524300, -13.39321520033831625 ) ) ;
#27532=ORIENTED_EDGE ( 'NONE', *, *, #41310, .F. ) ;
#27535=CARTESIAN_POINT ( 'NONE',  ( 89.12784890491134604, -27.84333996136784961, -14.15691383771150136 ) ) ;
#27538=EDGE_CURVE ( 'NONE', #39963, #30333, #36462, .T. ) ;
#27573=EDGE_LOOP ( 'NONE', ( #27949, #32643, #9869, #42514 ) ) ;
#27576=DIRECTION ( 'NONE',  ( -1.000000000000000000, 0.000000000000000000, 0.000000000000000000 ) ) ;
#27586=CARTESIAN_POINT ( 'NONE',  ( 90.72400676789006013, -25.99489077589524300, -13.39321520033831625 ) ) ;
#27606=VERTEX_POINT ( 'NONE', #31204 ) ;
#27629=CIRCLE ( 'NONE', #7947, 2.000000000000000444 ) ;
#27631=CIRCLE ( 'NONE', #29072, 2.000000000000000444 ) ;
#27663=ORIENTED_EDGE ( 'NONE', *, *, #16129, .F. ) ;
#27677=CARTESIAN_POINT ( 'NONE',  ( 88.35093386163799778, -25.23119213852205789, -15.24166438581092109 ) ) ;
#27680=CIRCLE ( 'NONE', #11643, 2.200000000000001066 ) ;
#27688=CARTESIAN_POINT ( 'NONE',  ( 96.54708369096698561, -26.33989114581222424, -11.20947992683166916 ) ) ;
#27696=ORIENTED_EDGE ( 'NONE', *, *, #16701, .T. ) ;
#27701=CARTESIAN_POINT ( 'NONE',  ( 86.75477599865929790, -25.99489077589524300, -13.39321520033831625 ) ) ;
#27705=AXIS2_PLACEMENT_3D ( 'NONE', #19430, #9175, #10527 ) ;
#27718=DIRECTION ( 'NONE',  ( 0.000000000000000000, -0.3818493186865936084, 0.9242245927363024194 ) ) ;
#27739=AXIS2_PLACEMENT_3D ( 'NONE', #5009, #39903, #33264 ) ;
#27747=FACE_OUTER_BOUND ( 'NONE', #23297, .T. ) ;
#27751=AXIS2_PLACEMENT_3D ( 'NONE', #4867, #8077, #29046 ) ;
#27758=FACE_OUTER_BOUND ( 'NONE', #17218, .T. ) ;
#27766=FACE_OUTER_BOUND ( 'NONE', #7067, .T. ) ;
#27769=DIRECTION ( 'NONE',  ( 1.000000000000000000, 0.000000000000000000, 0.000000000000000000 ) ) ;
#27775=ORIENTED_EDGE ( 'NONE', *, *, #2542, .F. ) ;
#27789=ORIENTED_EDGE ( 'NONE', *, *, #13360, .F. ) ;
#27823=ORIENTED_EDGE ( 'NONE', *, *, #35587, .F. ) ;
#27850=CIRCLE ( 'NONE', #8180, 6.479565957685750277 ) ;
#27897=PLANE ( 'NONE',  #14227 ) ;
#27901=EDGE_CURVE ( 'NONE', #33593, #25225, #45097, .T. ) ;
#27903=ORIENTED_EDGE ( 'NONE', *, *, #13435, .F. ) ;
#27921=CARTESIAN_POINT ( 'NONE',  ( 85.15861813568058380, -25.23119213852205789, -15.24166438581092109 ) ) ;
#27948=ADVANCED_FACE ( 'NONE', ( #30958 ), #13854, .T. ) ;
#27949=ORIENTED_EDGE ( 'NONE', *, *, #10180, .F. ) ;
#27950=VECTOR ( 'NONE', #43249, 1000.000000000000000 ) ;
#27956=ORIENTED_EDGE ( 'NONE', *, *, #41804, .F. ) ;
#27958=CIRCLE ( 'NONE', #33760, 2.000000000000000444 ) ;
#27964=DIRECTION ( 'NONE',  ( -0.4461977533474357216, -0.8271203734159378040, -0.3417300876246930907 ) ) ;
#27968=CARTESIAN_POINT ( 'NONE',  ( 96.46827370896536991, -26.60028948451273223, -14.20056342530837412 ) ) ;
#27979=DIRECTION ( 'NONE',  ( 1.000000000000000000, 0.000000000000000000, -0.000000000000000000 ) ) ;
#27984=FACE_OUTER_BOUND ( 'NONE', #35074, .T. ) ;
#27987=DIRECTION ( 'NONE',  ( 0.000000000000000000, -0.3818493186865927203, 0.9242245927363029745 ) ) ;
#27991=CYLINDRICAL_SURFACE ( 'NONE', #42024, 1.999999999999998890 ) ;
#27993=DIRECTION ( 'NONE',  ( 0.000000000000000000, -0.3818493186865927203, 0.9242245927363029745 ) ) ;
#28009=EDGE_CURVE ( 'NONE', #14596, #36351, #18963, .T. ) ;
#28053=FACE_OUTER_BOUND ( 'NONE', #2728, .T. ) ;
#28153=EDGE_CURVE ( 'NONE', #19198, #2194, #14568, .T. ) ;
#28156=DIRECTION ( 'NONE',  ( 0.000000000000000000, -0.3818493186865936084, 0.9242245927363024194 ) ) ;
#28172=AXIS2_PLACEMENT_3D ( 'NONE', #26214, #8213, #36905 ) ;
#28182=AXIS2_PLACEMENT_3D ( 'NONE', #35594, #18735, #31732 ) ;
#28186=CONICAL_SURFACE ( 'NONE', #2689, 2.000000000000000444, 0.9599310885968830309 ) ;
#28187=CARTESIAN_POINT ( 'NONE',  ( 87.80477198183443477, -25.99489077589524300, -13.39321520033831625 ) ) ;
#28191=DIRECTION ( 'NONE',  ( 1.000000000000000000, 0.000000000000000000, -0.000000000000000000 ) ) ;
#28234=DIRECTION ( 'NONE',  ( 0.000000000000000000, -0.9242245927363028635, -0.3818493186865930533 ) ) ;
#28241=CONICAL_SURFACE ( 'NONE', #40615, 1.610000000000000986, 0.9599310885968765916 ) ;
#28250=FACE_OUTER_BOUND ( 'NONE', #14930, .T. ) ;
#28252=LINE ( 'NONE', #18662, #41666 ) ;
#28258=DIRECTION ( 'NONE',  ( 1.000000000000000000, 0.000000000000000000, -0.000000000000000000 ) ) ;
#28262=VERTEX_POINT ( 'NONE', #14077 ) ;
#28265=CARTESIAN_POINT ( 'NONE',  ( 87.68939540009954214, -25.23119213852205789, -15.24166438581092109 ) ) ;
#28298=LINE ( 'NONE', #41987, #3347 ) ;
#28337=VERTEX_POINT ( 'NONE', #4250 ) ;
#28339=DIRECTION ( 'NONE',  ( 0.000000000000000000, -0.3818493186865927203, 0.9242245927363029745 ) ) ;
#28342=ORIENTED_EDGE ( 'NONE', *, *, #19486, .T. ) ;
#28348=ORIENTED_EDGE ( 'NONE', *, *, #11927, .F. ) ;
#28356=ORIENTED_EDGE ( 'NONE', *, *, #5258, .F. ) ;
#28371=DIRECTION ( 'NONE',  ( -0.5735764363510450492, -0.3127926500124816878, 0.7570804645221038687 ) ) ;
#28374=ORIENTED_EDGE ( 'NONE', *, *, #13019, .F. ) ;
#28395=ADVANCED_FACE ( 'NONE', ( #15647 ), #18213, .T. ) ;
#28408=DIRECTION ( 'NONE',  ( -0.5735764363510446051, 0.3127926500124816878, -0.7570804645221042017 ) ) ;
#28415=LINE ( 'NONE', #14059, #15838 ) ;
#28442=VERTEX_POINT ( 'NONE', #4923 ) ;
#28452=ADVANCED_FACE ( 'NONE', ( #40498 ), #7338, .T. ) ;
#28457=ORIENTED_EDGE ( 'NONE', *, *, #38798, .F. ) ;
#28464=DIRECTION ( 'NONE',  ( 1.000000000000000000, 0.000000000000000000, -0.000000000000000000 ) ) ;
#28465=CONICAL_SURFACE ( 'NONE', #37931, 2.000000000000000444, 0.9599310885968830309 ) ;
#28486=CARTESIAN_POINT ( 'NONE',  ( 94.20708369096698220, -25.56540164683820393, -12.65854514648976981 ) ) ;
#28507=DIRECTION ( 'NONE',  ( 0.000000000000000000, -0.3818493186865936084, 0.9242245927363024194 ) ) ;
#28519=CARTESIAN_POINT ( 'NONE',  ( 94.20708369096698220, -25.99489077589524300, -13.39321520033831447 ) ) ;
#28523=EDGE_CURVE ( 'NONE', #25112, #33401, #9531, .T. ) ;
#28535=EDGE_LOOP ( 'NONE', ( #3108, #26849, #1701, #15931, #26024, #9879 ) ) ;
#28540=AXIS2_PLACEMENT_3D ( 'NONE', #42621, #11384, #32114 ) ;
#28548=DIRECTION ( 'NONE',  ( 1.000000000000000000, 0.000000000000000000, -0.000000000000000000 ) ) ;
#28556=DIRECTION ( 'NONE',  ( 1.000000000000000000, 0.000000000000000000, -0.000000000000000000 ) ) ;
#28563=ORIENTED_EDGE ( 'NONE', *, *, #7465, .T. ) ;
#28604=ORIENTED_EDGE ( 'NONE', *, *, #6417, .T. ) ;
#28606=DIRECTION ( 'NONE',  ( 0.000000000000000000, -0.3818493186865927203, 0.9242245927363029745 ) ) ;
#28628=CARTESIAN_POINT ( 'NONE',  ( 86.48169505875749508, -25.23119213852205789, -15.24166438581092109 ) ) ;
#28673=AXIS2_PLACEMENT_3D ( 'NONE', #32747, #19537, #26605 ) ;
#28710=FACE_OUTER_BOUND ( 'NONE', #44738, .T. ) ;
#28712=CARTESIAN_POINT ( 'NONE',  ( 91.77400275106518279, -25.23119213852205789, -15.24166438581092109 ) ) ;
#28716=DIRECTION ( 'NONE',  ( 0.000000000000000000, -0.9242245927363027524, -0.3818493186865928868 ) ) ;
#28729=EDGE_CURVE ( 'NONE', #2441, #28337, #43021, .T. ) ;
#28731=DIRECTION ( 'NONE',  ( 0.5735764363510499342, 0.3127926500124801890, -0.7570804645221008711 ) ) ;
#28733=ORIENTED_EDGE ( 'NONE', *, *, #38422, .T. ) ;
#28737=ORIENTED_EDGE ( 'NONE', *, *, #10023, .T. ) ;
#28750=CARTESIAN_POINT ( 'NONE',  ( 90.48265143217095385, -25.66130191030491758, -14.20063063452593255 ) ) ;
#28756=CARTESIAN_POINT ( 'NONE',  ( 92.04708369096698561, -25.99489077589524300, -13.39321520033831625 ) ) ;
#28760=DIRECTION ( 'NONE',  ( 0.000000000000000000, -0.3818493186865927203, 0.9242245927363029745 ) ) ;
#28770=CARTESIAN_POINT ( 'NONE',  ( 94.20708369096698220, -26.09538666226425363, -14.49867541642786861 ) ) ;
#28790=DIRECTION ( 'NONE',  ( 0.000000000000000000, -0.3818493186865927203, 0.9242245927363029745 ) ) ;
#28802=CARTESIAN_POINT ( 'NONE',  ( 92.04708369096698561, -25.38011337280982715, -14.88121679464376257 ) ) ;
#28803=EDGE_LOOP ( 'NONE', ( #26643, #40866, #18292, #27054, #14773 ) ) ;
#28813=VECTOR ( 'NONE', #21267, 1000.000000000000114 ) ;
#28821=DIRECTION ( 'NONE',  ( -0.4461977533474357771, 0.3417300876246960328, -0.8271203734159368048 ) ) ;
#28832=EDGE_CURVE ( 'NONE', #35171, #5517, #29905, .T. ) ;
#28836=CYLINDRICAL_SURFACE ( 'NONE', #1433, 1.999999999999998890 ) ;
#28856=AXIS2_PLACEMENT_3D ( 'NONE', #12859, #16502, #29948 ) ;
#28863=CARTESIAN_POINT ( 'NONE',  ( 93.44708369096697709, -25.99489077589524300, -13.39321520033831447 ) ) ;
#28875=AXIS2_PLACEMENT_3D ( 'NONE', #42041, #11480, #13995 ) ;
#28904=CARTESIAN_POINT ( 'NONE',  ( 94.20708369096698220, -26.84634622004463012, -12.68105978249595189 ) ) ;
#28944=ORIENTED_EDGE ( 'NONE', *, *, #12244, .F. ) ;
#28954=ORIENTED_EDGE ( 'NONE', *, *, #32524, .F. ) ;
#28963=EDGE_CURVE ( 'NONE', #9582, #42332, #1954, .T. ) ;
#28968=CARTESIAN_POINT ( 'NONE',  ( 87.02785693856107230, -25.99489077589524300, -13.39321520033831447 ) ) ;
#28971=EDGE_CURVE ( 'NONE', #26936, #26522, #44378, .T. ) ;
#29040=CARTESIAN_POINT ( 'NONE',  ( 96.46827370896536991, -26.13949388144357755, -14.39191870720298994 ) ) ;
#29046=DIRECTION ( 'NONE',  ( 0.000000000000000000, -0.3818493186865936084, 0.9242245927363024194 ) ) ;
#29067=DIRECTION ( 'NONE',  ( 0.000000000000000000, -0.9242245927363029745, -0.3818493186865929978 ) ) ;
#29072=AXIS2_PLACEMENT_3D ( 'NONE', #23611, #3071, #10595 ) ;
#29096=DIRECTION ( 'NONE',  ( 0.000000000000000000, -0.3818493186865936084, 0.9242245927363024194 ) ) ;
#29108=ORIENTED_EDGE ( 'NONE', *, *, #38421, .T. ) ;
#29122=AXIS2_PLACEMENT_3D ( 'NONE', #2427, #37309, #23422 ) ;
#29152=ORIENTED_EDGE ( 'NONE', *, *, #1593, .T. ) ;
#29156=FACE_OUTER_BOUND ( 'NONE', #36218, .T. ) ;
#29160=CARTESIAN_POINT ( 'NONE',  ( 96.21525317080913453, -27.63241331390002031, -14.62699200570882851 ) ) ;
#29166=ORIENTED_EDGE ( 'NONE', *, *, #11363, .T. ) ;
#29169=AXIS2_PLACEMENT_3D ( 'NONE', #315, #35631, #22188 ) ;
#29182=CARTESIAN_POINT ( 'NONE',  ( 121.9470836909669913, -24.14644159042263993, -12.62951656296512937 ) ) ;
#29194=LINE ( 'NONE', #33040, #44422 ) ;
#29218=AXIS2_PLACEMENT_3D ( 'NONE', #10283, #16281, #41961 ) ;
#29227=ORIENTED_EDGE ( 'NONE', *, *, #16988, .T. ) ;
#29233=EDGE_LOOP ( 'NONE', ( #39093, #1677, #45012, #34517, #33454, #20048 ) ) ;
#29243=LINE ( 'NONE', #19426, #7600 ) ;
#29245=ORIENTED_EDGE ( 'NONE', *, *, #16356, .F. ) ;
#29280=EDGE_LOOP ( 'NONE', ( #27191, #32274, #37473, #12838 ) ) ;
#29306=DIRECTION ( 'NONE',  ( 0.000000000000000000, -0.3818493186865936084, 0.9242245927363024194 ) ) ;
#29308=DIRECTION ( 'NONE',  ( 0.000000000000000000, -0.3818493186865936084, 0.9242245927363024194 ) ) ;
#29364=DIRECTION ( 'NONE',  ( 0.000000000000000000, -0.3818493186865927203, 0.9242245927363029745 ) ) ;
#29371=ORIENTED_EDGE ( 'NONE', *, *, #7588, .T. ) ;
#29375=DIRECTION ( 'NONE',  ( -1.000000000000000000, 0.000000000000000000, 0.000000000000000000 ) ) ;
#29384=DIRECTION ( 'NONE',  ( -1.000000000000000000, 0.000000000000000000, 0.000000000000000000 ) ) ;
#29386=ORIENTED_EDGE ( 'NONE', *, *, #36785, .T. ) ;
#29390=EDGE_CURVE ( 'NONE', #31284, #39770, #38620, .T. ) ;
#29400=EDGE_LOOP ( 'NONE', ( #4624, #2096, #34320, #4609, #21461 ) ) ;
#29406=VERTEX_POINT ( 'NONE', #35658 ) ;
#29447=( GEOMETRIC_REPRESENTATION_CONTEXT ( 3 ) GLOBAL_UNCERTAINTY_ASSIGNED_CONTEXT ( ( #42467 ) ) GLOBAL_UNIT_ASSIGNED_CONTEXT ( ( #25819, #16244, #33312 ) ) REPRESENTATION_CONTEXT ( 'NONE', 'WORKASPACE' ) );
#29473=EDGE_CURVE ( 'NONE', #26936, #42171, #753, .T. ) ;
#29477=DIRECTION ( 'NONE',  ( 1.000000000000000000, 0.000000000000000000, -0.000000000000000000 ) ) ;
#29490=VECTOR ( 'NONE', #13344, 1000.000000000000114 ) ;
#29499=DIRECTION ( 'NONE',  ( 0.000000000000000000, -0.3818493186865936084, 0.9242245927363024194 ) ) ;
#29519=CARTESIAN_POINT ( 'NONE',  ( 85.70478001548416103, -25.99489077589524300, -13.39321520033831447 ) ) ;
#29526=LINE ( 'NONE', #1923, #32301 ) ;
#29532=FACE_OUTER_BOUND ( 'NONE', #19143, .T. ) ;
#29539=CARTESIAN_POINT ( 'NONE',  ( 91.11246428952674137, -24.14644159042263993, -12.62951656296512937 ) ) ;
#29557=DIRECTION ( 'NONE',  ( 1.000000000000000000, 0.000000000000000000, -0.000000000000000000 ) ) ;
#29570=AXIS2_PLACEMENT_3D ( 'NONE', #14691, #17887, #28606 ) ;
#29572=ORIENTED_EDGE ( 'NONE', *, *, #34615, .F. ) ;
#29578=FACE_OUTER_BOUND ( 'NONE', #29400, .T. ) ;
#29581=CARTESIAN_POINT ( 'NONE',  ( 92.32016463086877422, -25.99489077589524300, -13.39321520033831447 ) ) ;
#29600=DIRECTION ( 'NONE',  ( 0.000000000000000000, -0.9242245927363028635, -0.3818493186865930533 ) ) ;
#29622=CARTESIAN_POINT ( 'NONE',  ( 87.14323352029596492, -25.99489077589524300, -13.39321520033831625 ) ) ;
#29623=VERTEX_POINT ( 'NONE', #22209 ) ;
#29637=CARTESIAN_POINT ( 'NONE',  ( 89.01247232317646763, -26.75858941326842810, -11.54476601486570964 ) ) ;
#29652=CARTESIAN_POINT ( 'NONE',  ( 87.80477198183443477, -25.23119213852205789, -15.24166438581092109 ) ) ;
#29653=B_SPLINE_CURVE_WITH_KNOTS ( 'NONE', 3,
 ( #13921, #10506, #34205, #34424 ),
 .UNSPECIFIED., .F., .F.,
 ( 4, 4 ),
 ( 0.000000000000000000, 1.000000000000000000 ),
 .UNSPECIFIED. ) ;
#29665=CARTESIAN_POINT ( 'NONE',  ( 90.45092582798827152, -25.99489077589524300, -13.39321520033831625 ) ) ;
#29671=CARTESIAN_POINT ( 'NONE',  ( 85.70478001548416103, -24.14644159042263993, -12.62951656296512937 ) ) ;
#29678=ORIENTED_EDGE ( 'NONE', *, *, #12476, .T. ) ;
#29684=ORIENTED_EDGE ( 'NONE', *, *, #22078, .F. ) ;
#29689=VERTEX_POINT ( 'NONE', #4876 ) ;
#29703=CARTESIAN_POINT ( 'NONE',  ( 91.77400275106518279, -26.75858941326842810, -11.54476601486570964 ) ) ;
#29708=PLANE ( 'NONE',  #5052 ) ;
#29729=CIRCLE ( 'NONE', #17371, 2.000000000000000444 ) ;
#29732=DIRECTION ( 'NONE',  ( 0.000000000000000000, -0.3818493186865927203, 0.9242245927363029745 ) ) ;
#29753=ADVANCED_FACE ( 'NONE', ( #25643 ), #21988, .T. ) ;
#29759=EDGE_LOOP ( 'NONE', ( #36878, #15702, #31274, #19084 ) ) ;
#29779=FACE_OUTER_BOUND ( 'NONE', #25532, .T. ) ;
#29792=EDGE_CURVE ( 'NONE', #44542, #5526, #8097, .T. ) ;
#29802=CARTESIAN_POINT ( 'NONE',  ( 87.68939540009954214, -26.75858941326842810, -11.54476601486570964 ) ) ;
#29830=AXIS2_PLACEMENT_3D ( 'NONE', #32338, #7057, #38275 ) ;
#29846=ADVANCED_FACE ( 'NONE', ( #28053 ), #791, .T. ) ;
#29859=AXIS2_PLACEMENT_3D ( 'NONE', #21693, #6891, #10765 ) ;
#29880=CARTESIAN_POINT ( 'NONE',  ( 96.46827370896536991, -25.99489077589524300, -13.39321520033831447 ) ) ;
#29892=ORIENTED_EDGE ( 'NONE', *, *, #7463, .T. ) ;
#29905=CIRCLE ( 'NONE', #38632, 2.000000000000000444 ) ;
#29915=ORIENTED_EDGE ( 'NONE', *, *, #3612, .T. ) ;
#29916=ORIENTED_EDGE ( 'NONE', *, *, #44807, .T. ) ;
#29941=FACE_OUTER_BOUND ( 'NONE', #29759, .T. ) ;
#29948=DIRECTION ( 'NONE',  ( 0.000000000000000000, -0.3818493186865927203, 0.9242245927363029745 ) ) ;
#29974=CARTESIAN_POINT ( 'NONE',  ( 96.46827370896536991, -24.99618726903056753, -13.53781830588664903 ) ) ;
#29978=ORIENTED_EDGE ( 'NONE', *, *, #41810, .F. ) ;
#29988=ORIENTED_EDGE ( 'NONE', *, *, #21144, .T. ) ;
#29997=DIRECTION ( 'NONE',  ( 1.000000000000000000, 0.000000000000000000, -0.000000000000000000 ) ) ;
#30019=AXIS2_PLACEMENT_3D ( 'NONE', #18772, #29477, #14282 ) ;
#30024=APPLICATION_CONTEXT ( 'automotive_design' ) ;
#30028=DIRECTION ( 'NONE',  ( 0.000000000000000000, -0.9242245927363027524, -0.3818493186865929423 ) ) ;
#30029=AXIS2_PLACEMENT_3D ( 'NONE', #40574, #27115, #26439 ) ;
#30030=DIRECTION ( 'NONE',  ( 1.000000000000000000, 0.000000000000000000, -0.000000000000000000 ) ) ;
#30040=EDGE_CURVE ( 'NONE', #12514, #7405, #33551, .T. ) ;
#30047=EDGE_CURVE ( 'NONE', #14434, #10139, #14639, .T. ) ;
#30077=EDGE_CURVE ( 'NONE', #7733, #35058, #13926, .T. ) ;
#30080=ORIENTED_EDGE ( 'NONE', *, *, #5785, .F. ) ;
#30087=AXIS2_PLACEMENT_3D ( 'NONE', #22802, #25341, #28760 ) ;
#30109=FACE_OUTER_BOUND ( 'NONE', #44395, .T. ) ;
#30114=CARTESIAN_POINT ( 'NONE',  ( 121.9470836909669913, -25.99489077589524300, -13.39321520033831447 ) ) ;
#30125=CIRCLE ( 'NONE', #32916, 0.3599999999999998201 ) ;
#30142=EDGE_LOOP ( 'NONE', ( #34871, #7574, #20092, #44985, #36236 ) ) ;
#30143=EDGE_LOOP ( 'NONE', ( #3262, #39638, #501, #32714, #4289, #44128 ) ) ;
#30148=CYLINDRICAL_SURFACE ( 'NONE', #40336, 1.999999999999998890 ) ;
#30156=EDGE_LOOP ( 'NONE', ( #5633, #41808, #22755, #34567, #6390 ) ) ;
#30203=FACE_BOUND ( 'NONE', #7545, .T. ) ;
#30207=VERTEX_POINT ( 'NONE', #41888 ) ;
#30216=ADVANCED_FACE ( 'NONE', ( #37780 ), #38668, .T. ) ;
#30219=DIRECTION ( 'NONE',  ( 0.000000000000000000, -0.3818493186865897226, 0.9242245927363041957 ) ) ;
#30220=CARTESIAN_POINT ( 'NONE',  ( 121.9470836909669913, -25.99489077589524300, -13.39321520033831447 ) ) ;
#30262=CARTESIAN_POINT ( 'NONE',  ( 86.75477599865929790, -25.38011337280982715, -14.88121679464376257 ) ) ;
#30298=DIRECTION ( 'NONE',  ( 0.5735764363510498232, -0.3127926500124802445, 0.7570804645221007600 ) ) ;
#30324=ORIENTED_EDGE ( 'NONE', *, *, #10023, .F. ) ;
#30327=ADVANCED_FACE ( 'NONE', ( #27984 ), #27050, .T. ) ;
#30333=VERTEX_POINT ( 'NONE', #27535 ) ;
#30337=EDGE_CURVE ( 'NONE', #21796, #22202, #4442, .T. ) ;
#30339=CIRCLE ( 'NONE', #35431, 2.000000000000000444 ) ;
#30341=ADVANCED_FACE ( 'NONE', ( #27758 ), #1535, .T. ) ;
#30344=ORIENTED_EDGE ( 'NONE', *, *, #38422, .F. ) ;
#30360=EDGE_CURVE ( 'NONE', #8497, #39217, #44414, .T. ) ;
#30403=DIRECTION ( 'NONE',  ( 0.000000000000000000, -0.9242245927363029745, -0.3818493186865925537 ) ) ;
#30434=CARTESIAN_POINT ( 'NONE',  ( 88.73939138327467901, -26.60966817898065884, -11.90521360603286816 ) ) ;
#30450=DIRECTION ( 'NONE',  ( 1.000000000000000000, 0.000000000000000000, -0.000000000000000000 ) ) ;
#30451=CARTESIAN_POINT ( 'NONE',  ( 88.46631044337289040, -25.23119213852205789, -15.24166438581092109 ) ) ;
#30467=ORIENTED_EDGE ( 'NONE', *, *, #31477, .F. ) ;
#30475=ORIENTED_EDGE ( 'NONE', *, *, #22817, .F. ) ;
#30485=CARTESIAN_POINT ( 'NONE',  ( 88.35093386163799778, -25.99489077589524300, -13.39321520033831447 ) ) ;
#30487=EDGE_CURVE ( 'NONE', #1042, #10767, #43399, .T. ) ;
#30498=DIRECTION ( 'NONE',  ( 0.000000000000000000, -0.9242245927363040847, -0.3818493186865897226 ) ) ;
#30502=LINE ( 'NONE', #22986, #18956 ) ;
#30512=CARTESIAN_POINT ( 'NONE',  ( 87.02785693856107230, -25.99489077589524300, -13.39321520033831447 ) ) ;
#30524=DIRECTION ( 'NONE',  ( 1.000000000000000000, 0.000000000000000000, -0.000000000000000000 ) ) ;
#30538=CIRCLE ( 'NONE', #15999, 6.479565957685756494 ) ;
#30543=VECTOR ( 'NONE', #14910, 1000.000000000000000 ) ;
#30548=ORIENTED_EDGE ( 'NONE', *, *, #42966, .F. ) ;
#30579=ORIENTED_EDGE ( 'NONE', *, *, #32648, .F. ) ;
#30585=EDGE_CURVE ( 'NONE', #18037, #4544, #6672, .T. ) ;
#30593=FACE_OUTER_BOUND ( 'NONE', #7137, .T. ) ;
#30603=VERTEX_POINT ( 'NONE', #40892 ) ;
#30611=AXIS2_PLACEMENT_3D ( 'NONE', #10052, #2962, #6396 ) ;
#30618=CARTESIAN_POINT ( 'NONE',  ( 90.04708369096697140, -25.79823837677164988, -13.86919086559751157 ) ) ;
#30620=EDGE_CURVE ( 'NONE', #26284, #37865, #25610, .T. ) ;
#30632=AXIS2_PLACEMENT_3D ( 'NONE', #42433, #11197, #32150 ) ;
#30668=ORIENTED_EDGE ( 'NONE', *, *, #38003, .T. ) ;
#30680=CONICAL_SURFACE ( 'NONE', #38651, 1.610000000000000986, 0.9599310885968765916 ) ;
#30731=CARTESIAN_POINT ( 'NONE',  ( 90.72400676789006013, -25.99489077589524300, -13.39321520033831625 ) ) ;
#30736=DIRECTION ( 'NONE',  ( 0.000000000000000000, -0.3818493186865927203, 0.9242245927363029745 ) ) ;
#30740=DIRECTION ( 'NONE',  ( 0.000000000000000000, -0.9242245927363005320, -0.3818493186865984379 ) ) ;
#30753=CARTESIAN_POINT ( 'NONE',  ( 88.46631044337289040, -27.84333996136784961, -14.15691383771150136 ) ) ;
#30758=EDGE_LOOP ( 'NONE', ( #26546, #43835, #15728, #8078 ) ) ;
#30781=CARTESIAN_POINT ( 'NONE',  ( 96.54708369096698561, -25.64989040597826175, -15.57695047384496156 ) ) ;
#30782=EDGE_CURVE ( 'NONE', #26522, #20212, #37237, .T. ) ;
#30783=CARTESIAN_POINT ( 'NONE',  ( 83.44708369096697709, -25.23119213852205789, -15.24166438581092109 ) ) ;
#30793=VERTEX_POINT ( 'NONE', #38786 ) ;
#30803=LINE ( 'NONE', #3870, #20527 ) ;
#30815=AXIS2_PLACEMENT_3D ( 'NONE', #35442, #29067, #1024 ) ;
#30816=ORIENTED_EDGE ( 'NONE', *, *, #19032, .F. ) ;
#30823=LINE ( 'NONE', #27413, #20797 ) ;
#30850=VECTOR ( 'NONE', #42141, 1000.000000000000000 ) ;
#30859=VERTEX_POINT ( 'NONE', #7789 ) ;
#30872=EDGE_CURVE ( 'NONE', #34542, #22604, #21472, .T. ) ;
#30879=DIRECTION ( 'NONE',  ( 0.000000000000000000, -0.9242245927363029745, -0.3818493186865927758 ) ) ;
#30932=DIRECTION ( 'NONE',  ( 1.000000000000000000, 0.000000000000000000, -0.000000000000000000 ) ) ;
#30937=DIRECTION ( 'NONE',  ( 1.000000000000000000, 0.000000000000000000, -0.000000000000000000 ) ) ;
#30950=CARTESIAN_POINT ( 'NONE',  ( 87.68939540009954214, -25.99489077589524300, -13.39321520033831447 ) ) ;
#30955=CARTESIAN_POINT ( 'NONE',  ( 96.21525317080913453, -27.22866758126576059, -11.75569266233354426 ) ) ;
#30958=FACE_OUTER_BOUND ( 'NONE', #27573, .T. ) ;
#30965=CONICAL_SURFACE ( 'NONE', #14915, 2.000000000000000444, 0.9599310885968830309 ) ;
#30973=ADVANCED_FACE ( 'NONE', ( #1385 ), #1827, .T. ) ;
#31006=CARTESIAN_POINT ( 'NONE',  ( 87.80477198183443477, -25.23119213852205789, -15.24166438581092109 ) ) ;
#31018=LINE ( 'NONE', #27386, #5274 ) ;
#31020=EDGE_LOOP ( 'NONE', ( #33468, #12467, #5472, #40943 ) ) ;
#31021=CIRCLE ( 'NONE', #11366, 6.426280380454326036 ) ;
#31025=ORIENTED_EDGE ( 'NONE', *, *, #2542, .T. ) ;
#31031=ORIENTED_EDGE ( 'NONE', *, *, #24530, .T. ) ;
#31032=ORIENTED_EDGE ( 'NONE', *, *, #2823, .T. ) ;
#31034=ADVANCED_FACE ( 'NONE', ( #18727 ), #19058, .T. ) ;
#31035=CIRCLE ( 'NONE', #28182, 6.426280380454326036 ) ;
#31036=DIRECTION ( 'NONE',  ( 0.000000000000000000, -0.3818493186865927203, 0.9242245927363029745 ) ) ;
#31060=DIRECTION ( 'NONE',  ( 0.000000000000000000, -0.3818493186865936084, 0.9242245927363024194 ) ) ;
#31067=ORIENTED_EDGE ( 'NONE', *, *, #31968, .F. ) ;
#31077=VERTEX_POINT ( 'NONE', #26018 ) ;
#31083=EDGE_LOOP ( 'NONE', ( #14648, #31580, #19874, #8363 ) ) ;
#31114=AXIS2_PLACEMENT_3D ( 'NONE', #9741, #30030, #24100 ) ;
#31164=DIRECTION ( 'NONE',  ( 0.000000000000000000, -0.3818493186865936084, 0.9242245927363024194 ) ) ;
#31185=ORIENTED_EDGE ( 'NONE', *, *, #5500, .T. ) ;
#31198=DIRECTION ( 'NONE',  ( 0.000000000000000000, 0.3818493186865927203, -0.9242245927363029745 ) ) ;
#31203=CARTESIAN_POINT ( 'NONE',  ( 83.72016463086879412, -25.23119213852205789, -15.24166438581092109 ) ) ;
#31204=CARTESIAN_POINT ( 'NONE',  ( 90.45092582798827152, -26.75858941326842810, -11.54476601486570964 ) ) ;
#31222=VERTEX_POINT ( 'NONE', #43802 ) ;
#31223=DIRECTION ( 'NONE',  ( 1.000000000000000000, 0.000000000000000000, -0.000000000000000000 ) ) ;
#31264=CARTESIAN_POINT ( 'NONE',  ( 93.24708369096698846, -25.99489077589524300, -13.39321520033831447 ) ) ;
#31274=ORIENTED_EDGE ( 'NONE', *, *, #2285, .F. ) ;
#31284=VERTEX_POINT ( 'NONE', #26693 ) ;
#31285=DIRECTION ( 'NONE',  ( 0.000000000000000000, -0.9242245927363029745, -0.3818493186865927758 ) ) ;
#31297=CYLINDRICAL_SURFACE ( 'NONE', #32412, 1.999999999999998890 ) ;
#31321=AXIS2_PLACEMENT_3D ( 'NONE', #42125, #31843, #7904 ) ;
#31342=CARTESIAN_POINT ( 'NONE',  ( 95.62170725701132312, -26.92997340575169574, -13.22232672137451104 ) ) ;
#31350=CIRCLE ( 'NONE', #39366, 2.000000000000000444 ) ;
#31353=VERTEX_POINT ( 'NONE', #16663 ) ;
#31386=AXIS2_PLACEMENT_3D ( 'NONE', #24115, #17054, #23439 ) ;
#31391=VECTOR ( 'NONE', #4556, 1000.000000000000114 ) ;
#31408=CIRCLE ( 'NONE', #36516, 2.000000000000000444 ) ;
#31424=ADVANCED_FACE ( 'NONE', ( #9139 ), #16212, .T. ) ;
#31462=EDGE_CURVE ( 'NONE', #13605, #11206, #25064, .T. ) ;
#31471=ORIENTED_EDGE ( 'NONE', *, *, #12029, .F. ) ;
#31477=EDGE_CURVE ( 'NONE', #19939, #12295, #13988, .T. ) ;
#31480=CARTESIAN_POINT ( 'NONE',  ( 85.43169907558235820, -25.38011337280982715, -14.88121679464376257 ) ) ;
#31528=ORIENTED_EDGE ( 'NONE', *, *, #37844, .T. ) ;
#31533=VERTEX_POINT ( 'NONE', #24834 ) ;
#31544=DIRECTION ( 'NONE',  ( 0.000000000000000000, -0.3818493186865936084, 0.9242245927363024194 ) ) ;
#31546=CYLINDRICAL_SURFACE ( 'NONE', #29169, 1.999999999999998890 ) ;
#31547=CIRCLE ( 'NONE', #42501, 2.000000000000000444 ) ;
#31569=CARTESIAN_POINT ( 'NONE',  ( 92.04708369096698561, -25.99489077589524300, -13.39321520033831625 ) ) ;
#31572=ORIENTED_EDGE ( 'NONE', *, *, #29390, .F. ) ;
#31573=VECTOR ( 'NONE', #30298, 1000.000000000000114 ) ;
#31580=ORIENTED_EDGE ( 'NONE', *, *, #35841, .F. ) ;
#31582=AXIS2_PLACEMENT_3D ( 'NONE', #14496, #28191, #11304 ) ;
#31590=ADVANCED_FACE ( 'NONE', ( #39186 ), #8874, .T. ) ;
#31597=AXIS2_PLACEMENT_3D ( 'NONE', #13942, #17368, #468 ) ;
#31599=CARTESIAN_POINT ( 'NONE',  ( 90.04708369096697140, -26.19154317501883611, -12.91723953507911915 ) ) ;
#31600=DIRECTION ( 'NONE',  ( 0.000000000000000000, -0.3818493186865936084, 0.9242245927363024194 ) ) ;
#31610=CARTESIAN_POINT ( 'NONE',  ( 96.54708369096698561, -23.81115550238859413, -13.04821483042134389 ) ) ;
#31624=ORIENTED_EDGE ( 'NONE', *, *, #1121, .F. ) ;
#31637=LINE ( 'NONE', #37813, #16205 ) ;
#31642=DIRECTION ( 'NONE',  ( 1.000000000000000000, 0.000000000000000000, -0.000000000000000000 ) ) ;
#31650=DIRECTION ( 'NONE',  ( 0.000000000000000000, 0.3818493186865927203, -0.9242245927363029745 ) ) ;
#31660=CARTESIAN_POINT ( 'NONE',  ( 121.9470836909669913, -25.99489077589524300, -13.39321520033831447 ) ) ;
#31671=EDGE_LOOP ( 'NONE', ( #9110, #36070, #31989, #19392, #42712 ) ) ;
#31676=DIRECTION ( 'NONE',  ( 1.000000000000000000, 0.000000000000000000, -0.000000000000000000 ) ) ;
#31677=( LENGTH_UNIT ( ) NAMED_UNIT ( * ) SI_UNIT ( .MILLI., .METRE. ) );
#31681=DIRECTION ( 'NONE',  ( 0.000000000000000000, -0.3818493186865927203, 0.9242245927363029745 ) ) ;
#31685=VECTOR ( 'NONE', #39565, 1000.000000000000000 ) ;
#31692=AXIS2_PLACEMENT_3D ( 'NONE', #4377, #25808, #28790 ) ;
#31732=DIRECTION ( 'NONE',  ( 0.8949343913984424415, 0.4123869368673875324, 0.1703803081152070742 ) ) ;
#31746=CIRCLE ( 'NONE', #35374, 6.426280380454326924 ) ;
#31767=ORIENTED_EDGE ( 'NONE', *, *, #19432, .T. ) ;
#31772=CIRCLE ( 'NONE', #17954, 2.000000000000000444 ) ;
#31780=DIRECTION ( 'NONE',  ( 0.000000000000000000, -0.3818493186865936084, 0.9242245927363024194 ) ) ;
#31785=LINE ( 'NONE', #18112, #20852 ) ;
#31799=DIRECTION ( 'NONE',  ( -1.000000000000000000, 0.000000000000000000, 0.000000000000000000 ) ) ;
#31809=CARTESIAN_POINT ( 'NONE',  ( 86.48169505875749508, -25.99489077589524300, -13.39321520033831625 ) ) ;
#31810=AXIS2_PLACEMENT_3D ( 'NONE', #16275, #43862, #37220 ) ;
#31813=LINE ( 'NONE', #21560, #25869 ) ;
#31818=CIRCLE ( 'NONE', #9283, 2.000000000000000444 ) ;
#31833=EDGE_CURVE ( 'NONE', #23032, #18337, #13278, .T. ) ;
#31835=CARTESIAN_POINT ( 'NONE',  ( 93.24708369096698846, -25.99489077589524300, -13.39321520033831447 ) ) ;
#31841=CARTESIAN_POINT ( 'NONE',  ( 87.41631446019775353, -25.99489077589524300, -13.39321520033831625 ) ) ;
#31843=DIRECTION ( 'NONE',  ( 1.000000000000000000, 0.000000000000000000, -0.000000000000000000 ) ) ;
#31856=CIRCLE ( 'NONE', #2010, 2.200000000000001066 ) ;
#31869=CONICAL_SURFACE ( 'NONE', #12232, 1.610000000000000986, 0.9599310885968765916 ) ;
#31913=VERTEX_POINT ( 'NONE', #32332 ) ;
#31941=VERTEX_POINT ( 'NONE', #11374 ) ;
#31966=AXIS2_PLACEMENT_3D ( 'NONE', #41398, #34515, #44811 ) ;
#31967=DIRECTION ( 'NONE',  ( 0.000000000000000000, 0.3818493186865927203, -0.9242245927363029745 ) ) ;
#31968=EDGE_CURVE ( 'NONE', #19363, #42815, #28252, .T. ) ;
#31970=EDGE_CURVE ( 'NONE', #1522, #8271, #32165, .T. ) ;
#31973=ORIENTED_EDGE ( 'NONE', *, *, #5843, .T. ) ;
#31987=EDGE_CURVE ( 'NONE', #18337, #30859, #18354, .T. ) ;
#31989=ORIENTED_EDGE ( 'NONE', *, *, #31970, .T. ) ;
#32020=CARTESIAN_POINT ( 'NONE',  ( 89.78938736644981589, -25.99489077589524300, -13.39321520033831625 ) ) ;
#32048=ORIENTED_EDGE ( 'NONE', *, *, #8438, .F. ) ;
#32060=AXIS2_PLACEMENT_3D ( 'NONE', #6901, #20812, #24451 ) ;
#32068=DIRECTION ( 'NONE',  ( 0.5735764363510499342, 0.3127926500124801890, -0.7570804645221008711 ) ) ;
#32096=AXIS2_PLACEMENT_3D ( 'NONE', #18684, #21875, #25305 ) ;
#32110=LINE ( 'NONE', #35753, #6534 ) ;
#32114=DIRECTION ( 'NONE',  ( 0.000000000000000000, 0.3818493186865927203, -0.9242245927363029745 ) ) ;
#32129=DIRECTION ( 'NONE',  ( 1.000000000000000000, 0.000000000000000000, -0.000000000000000000 ) ) ;
#32133=ORIENTED_EDGE ( 'NONE', *, *, #11207, .F. ) ;
#32140=CARTESIAN_POINT ( 'NONE',  ( 92.04708369096698561, -25.38011337280982715, -14.88121679464376257 ) ) ;
#32148=CARTESIAN_POINT ( 'NONE',  ( 91.77400275106518279, -25.99489077589524300, -13.39321520033831625 ) ) ;
#32150=DIRECTION ( 'NONE',  ( 0.000000000000000000, 0.3818493186865927203, -0.9242245927363029745 ) ) ;
#32161=ORIENTED_EDGE ( 'NONE', *, *, #17851, .T. ) ;
#32165=CIRCLE ( 'NONE', #4504, 2.000000000000000444 ) ;
#32173=FACE_OUTER_BOUND ( 'NONE', #36335, .T. ) ;
#32177=DIRECTION ( 'NONE',  ( 0.000000000000000000, -0.3818493186865927203, 0.9242245927363029745 ) ) ;
#32183=DIRECTION ( 'NONE',  ( 1.000000000000000000, 0.000000000000000000, -0.000000000000000000 ) ) ;
#32191=ORIENTED_EDGE ( 'NONE', *, *, #39681, .F. ) ;
#32197=CIRCLE ( 'NONE', #30029, 2.000000000000000444 ) ;
#32202=STYLED_ITEM ( 'NONE', ( #14814 ), #15621 ) ;
#32205=LINE ( 'NONE', #14665, #25203 ) ;
#32228=LINE ( 'NONE', #17884, #12587 ) ;
#32231=AXIS2_PLACEMENT_3D ( 'NONE', #40522, #12030, #25933 ) ;
#32243=ORIENTED_EDGE ( 'NONE', *, *, #38937, .T. ) ;
#32248=ORIENTED_EDGE ( 'NONE', *, *, #2756, .T. ) ;
#32274=ORIENTED_EDGE ( 'NONE', *, *, #18105, .T. ) ;
#32284=CARTESIAN_POINT ( 'NONE',  ( 94.20708369096698220, -26.21217205256509075, -14.21600912764254687 ) ) ;
#32301=VECTOR ( 'NONE', #7880, 1000.000000000000000 ) ;
#32307=ADVANCED_FACE ( 'NONE', ( #25540 ), #26384, .F. ) ;
#32312=CARTESIAN_POINT ( 'NONE',  ( 88.46631044337289040, -25.23119213852205789, -15.24166438581092109 ) ) ;
#32325=DIRECTION ( 'NONE',  ( 1.000000000000000000, 0.000000000000000000, -0.000000000000000000 ) ) ;
#32332=CARTESIAN_POINT ( 'NONE',  ( 87.80477198183443477, -24.14644159042263993, -12.62951656296512937 ) ) ;
#32337=DIRECTION ( 'NONE',  ( 1.000000000000000000, 0.000000000000000000, -0.000000000000000000 ) ) ;
#32338=CARTESIAN_POINT ( 'NONE',  ( 121.9470836909669913, -25.99489077589524300, -13.39321520033831447 ) ) ;
#32343=CARTESIAN_POINT ( 'NONE',  ( 88.46631044337289040, -26.75858941326842810, -11.54476601486570964 ) ) ;
#32347=CIRCLE ( 'NONE', #24360, 2.000000000000000444 ) ;
#32349=ORIENTED_EDGE ( 'NONE', *, *, #34761, .F. ) ;
#32383=FACE_OUTER_BOUND ( 'NONE', #26530, .T. ) ;
#32392=ORIENTED_EDGE ( 'NONE', *, *, #5843, .F. ) ;
#32412=AXIS2_PLACEMENT_3D ( 'NONE', #37705, #38573, #24034 ) ;
#32457=AXIS2_PLACEMENT_3D ( 'NONE', #12682, #15871, #16091 ) ;
#32524=EDGE_CURVE ( 'NONE', #735, #44542, #32197, .T. ) ;
#32525=AXIS2_PLACEMENT_3D ( 'NONE', #33391, #43914, #29096 ) ;
#32538=CARTESIAN_POINT ( 'NONE',  ( 89.12784890491134604, -26.75858941326842810, -11.54476601486570964 ) ) ;
#32544=DIRECTION ( 'NONE',  ( 0.000000000000000000, -0.9242245927363028635, -0.3818493186865930533 ) ) ;
#32560=CARTESIAN_POINT ( 'NONE',  ( 87.68939540009954214, -24.14644159042263993, -12.62951656296512937 ) ) ;
#32571=ORIENTED_EDGE ( 'NONE', *, *, #6805, .T. ) ;
#32581=AXIS2_PLACEMENT_3D ( 'NONE', #4628, #18324, #4856 ) ;
#32595=DIRECTION ( 'NONE',  ( 0.000000000000000000, -0.3818493186865927203, 0.9242245927363029745 ) ) ;
#32599=DIRECTION ( 'NONE',  ( 0.000000000000000000, -0.3818493186865936084, 0.9242245927363024194 ) ) ;
#32603=CARTESIAN_POINT ( 'NONE',  ( 85.43169907558235820, -26.60966817898065884, -11.90521360603286816 ) ) ;
#32609=FACE_OUTER_BOUND ( 'NONE', #15708, .T. ) ;
#32621=CYLINDRICAL_SURFACE ( 'NONE', #24746, 1.999999999999998890 ) ;
#32643=ORIENTED_EDGE ( 'NONE', *, *, #9573, .F. ) ;
#32648=EDGE_CURVE ( 'NONE', #35146, #38132, #15482, .T. ) ;
#32665=EDGE_CURVE ( 'NONE', #43595, #1042, #35836, .T. ) ;
#32669=CARTESIAN_POINT ( 'NONE',  ( 96.54708369096698561, -28.17862604940189541, -13.73821557025528683 ) ) ;
#32686=ORIENTED_EDGE ( 'NONE', *, *, #43690, .T. ) ;
#32712=EDGE_CURVE ( 'NONE', #8271, #21347, #31637, .T. ) ;
#32714=ORIENTED_EDGE ( 'NONE', *, *, #3612, .F. ) ;
#32746=CARTESIAN_POINT ( 'NONE',  ( 96.21525317080913453, -24.35736823789046568, -12.15943839496780399 ) ) ;
#32747=CARTESIAN_POINT ( 'NONE',  ( 89.67401078471493747, -25.99489077589524300, -13.39321520033831447 ) ) ;
#32748=ORIENTED_EDGE ( 'NONE', *, *, #15069, .F. ) ;
#32760=FACE_OUTER_BOUND ( 'NONE', #42587, .T. ) ;
#32803=ADVANCED_FACE ( 'NONE', ( #17741 ), #40223, .T. ) ;
#32807=ORIENTED_EDGE ( 'NONE', *, *, #31462, .T. ) ;
#32815=DIRECTION ( 'NONE',  ( 0.000000000000000000, -0.3818493186865927203, 0.9242245927363029745 ) ) ;
#32824=ORIENTED_EDGE ( 'NONE', *, *, #10180, .T. ) ;
#32830=AXIS2_PLACEMENT_3D ( 'NONE', #43286, #19113, #25735 ) ;
#32836=CARTESIAN_POINT ( 'NONE',  ( 121.9470836909669913, -25.99489077589524300, -13.39321520033831447 ) ) ;
#32866=CARTESIAN_POINT ( 'NONE',  ( 85.82015659721905365, -26.75858941326842810, -11.54476601486570964 ) ) ;
#32867=ORIENTED_EDGE ( 'NONE', *, *, #33364, .T. ) ;
#32885=DIRECTION ( 'NONE',  ( 0.000000000000000000, -0.3818493186865927203, 0.9242245927363029745 ) ) ;
#32890=EDGE_LOOP ( 'NONE', ( #33826, #19271, #19553, #31185, #5415, #27956 ) ) ;
#32916=AXIS2_PLACEMENT_3D ( 'NONE', #26928, #5043, #12353 ) ;
#32919=VECTOR ( 'NONE', #23315, 1000.000000000000114 ) ;
#32925=VERTEX_POINT ( 'NONE', #39841 ) ;
#32929=CARTESIAN_POINT ( 'NONE',  ( 86.48169505875749508, -25.99489077589524300, -13.39321520033831625 ) ) ;
#32931=DIRECTION ( 'NONE',  ( 1.000000000000000000, 0.000000000000000000, -0.000000000000000000 ) ) ;
#32948=DIRECTION ( 'NONE',  ( 1.000000000000000000, 0.000000000000000000, -0.000000000000000000 ) ) ;
#32955=ORIENTED_EDGE ( 'NONE', *, *, #15006, .F. ) ;
#32956=CARTESIAN_POINT ( 'NONE',  ( 83.44708369096697709, -25.38011337280982715, -14.88121679464376257 ) ) ;
#32967=EDGE_CURVE ( 'NONE', #5058, #19198, #3843, .T. ) ;
#32970=ORIENTED_EDGE ( 'NONE', *, *, #8952, .F. ) ;
#32997=CYLINDRICAL_SURFACE ( 'NONE', #34990, 1.999999999999998890 ) ;
#33008=ORIENTED_EDGE ( 'NONE', *, *, #30040, .T. ) ;
#33020=DIRECTION ( 'NONE',  ( 0.000000000000000000, 0.3818493186865927203, -0.9242245927363029745 ) ) ;
#33029=CARTESIAN_POINT ( 'NONE',  ( 89.01247232317646763, -25.99489077589524300, -13.39321520033831447 ) ) ;
#33040=CARTESIAN_POINT ( 'NONE',  ( 86.48169505875749508, -25.23119213852205789, -15.24166438581092109 ) ) ;
#33051=ORIENTED_EDGE ( 'NONE', *, *, #8952, .T. ) ;
#33055=ADVANCED_FACE ( 'NONE', ( #36398 ), #1748, .T. ) ;
#33089=CARTESIAN_POINT ( 'NONE',  ( 94.20708369096698220, -25.99489077589524300, -13.39321520033831447 ) ) ;
#33102=CIRCLE ( 'NONE', #17134, 1.610000000000000986 ) ;
#33134=ORIENTED_EDGE ( 'NONE', *, *, #27538, .F. ) ;
#33141=CIRCLE ( 'NONE', #12051, 2.000000000000000444 ) ;
#33150=ORIENTED_EDGE ( 'NONE', *, *, #9845, .T. ) ;
#33157=CARTESIAN_POINT ( 'NONE',  ( 86.75477599865929790, -25.38011337280982715, -14.88121679464376257 ) ) ;
#33162=CARTESIAN_POINT ( 'NONE',  ( 96.21525317080913453, -24.76111397052472540, -15.03073773834309179 ) ) ;
#33181=ORIENTED_EDGE ( 'NONE', *, *, #39514, .F. ) ;
#33186=CONICAL_SURFACE ( 'NONE', #10658, 1.610000000000000986, 0.9599310885968765916 ) ;
#33189=DIRECTION ( 'NONE',  ( -1.224775218828351862E-16, 0.9242245927363029745, 0.3818493186865928868 ) ) ;
#33198=APPLICATION_CONTEXT ( 'automotive_design' ) ;
#33202=DIRECTION ( 'NONE',  ( 1.000000000000000000, 0.000000000000000000, -0.000000000000000000 ) ) ;
#33207=DIRECTION ( 'NONE',  ( 0.000000000000000000, -0.3818493186865927203, 0.9242245927363029745 ) ) ;
#33226=CARTESIAN_POINT ( 'NONE',  ( 83.44708369096697709, -25.99489077589524300, -13.39321520033831625 ) ) ;
#33229=DIRECTION ( 'NONE',  ( 1.000000000000000000, 0.000000000000000000, -0.000000000000000000 ) ) ;
#33247=AXIS2_PLACEMENT_3D ( 'NONE', #4047, #14103, #858 ) ;
#33261=DIRECTION ( 'NONE',  ( 1.000000000000000000, 0.000000000000000000, -0.000000000000000000 ) ) ;
#33264=DIRECTION ( 'NONE',  ( 0.000000000000000000, -0.3818493186865927203, 0.9242245927363029745 ) ) ;
#33305=AXIS2_PLACEMENT_3D ( 'NONE', #22685, #36583, #5359 ) ;
#33312=( NAMED_UNIT ( * ) SI_UNIT ( $, .STERADIAN. ) SOLID_ANGLE_UNIT ( ) );
#33349=ORIENTED_EDGE ( 'NONE', *, *, #6638, .F. ) ;
#33354=CIRCLE ( 'NONE', #19543, 0.1999999999999988731 ) ;
#33361=ADVANCED_FACE ( 'NONE', ( #39561 ), #21554, .T. ) ;
#33364=EDGE_CURVE ( 'NONE', #8089, #2933, #11870, .T. ) ;
#33368=DIRECTION ( 'NONE',  ( 1.000000000000000000, 0.000000000000000000, -0.000000000000000000 ) ) ;
#33373=ORIENTED_EDGE ( 'NONE', *, *, #3466, .F. ) ;
#33376=CYLINDRICAL_SURFACE ( 'NONE', #33305, 1.999999999999998890 ) ;
#33391=CARTESIAN_POINT ( 'NONE',  ( 88.07785292173620917, -25.99489077589524300, -13.39321520033831625 ) ) ;
#33401=VERTEX_POINT ( 'NONE', #28628 ) ;
#33420=DIRECTION ( 'NONE',  ( 0.5735764363510499342, 0.3127926500124801890, -0.7570804645221008711 ) ) ;
#33444=DIRECTION ( 'NONE',  ( 1.000000000000000000, 0.000000000000000000, -0.000000000000000000 ) ) ;
#33446=ORIENTED_EDGE ( 'NONE', *, *, #8696, .F. ) ;
#33454=ORIENTED_EDGE ( 'NONE', *, *, #29, .F. ) ;
#33456=CIRCLE ( 'NONE', #45146, 2.000000000000000444 ) ;
#33467=CARTESIAN_POINT ( 'NONE',  ( 121.9470836909669913, -25.99489077589524300, -13.39321520033831447 ) ) ;
#33468=ORIENTED_EDGE ( 'NONE', *, *, #45086, .T. ) ;
#33519=ORIENTED_EDGE ( 'NONE', *, *, #35056, .F. ) ;
#33532=ORIENTED_EDGE ( 'NONE', *, *, #16934, .T. ) ;
#33540=CIRCLE ( 'NONE', #43764, 2.000000000000000444 ) ;
#33551=CIRCLE ( 'NONE', #34287, 2.000000000000000444 ) ;
#33566=EDGE_LOOP ( 'NONE', ( #11577, #26313, #6636, #14571, #13044, #4039 ) ) ;
#33578=VERTEX_POINT ( 'NONE', #43207 ) ;
#33592=CARTESIAN_POINT ( 'NONE',  ( 88.07785292173620917, -25.99489077589524300, -13.39321520033831625 ) ) ;
#33593=VERTEX_POINT ( 'NONE', #12426 ) ;
#33618=AXIS2_PLACEMENT_3D ( 'NONE', #30114, #44030, #33739 ) ;
#33638=ORIENTED_EDGE ( 'NONE', *, *, #5225, .F. ) ;
#33643=CIRCLE ( 'NONE', #42427, 1.999999999999998890 ) ;
#33651=AXIS2_PLACEMENT_3D ( 'NONE', #6817, #6367, #31198 ) ;
#33653=CARTESIAN_POINT ( 'NONE',  ( 94.20708369096698220, -25.56540164683820393, -12.65854514648976981 ) ) ;
#33658=ADVANCED_FACE ( 'NONE', ( #26553 ), #8975, .T. ) ;
#33663=ORIENTED_EDGE ( 'NONE', *, *, #24193, .F. ) ;
#33670=AXIS2_PLACEMENT_3D ( 'NONE', #20320, #2752, #16677 ) ;
#33676=CONICAL_SURFACE ( 'NONE', #10405, 1.610000000000000986, 0.9599310885968765916 ) ;
#33686=ADVANCED_FACE ( 'NONE', ( #23360 ), #40248, .T. ) ;
#33687=EDGE_CURVE ( 'NONE', #20823, #5058, #12597, .T. ) ;
#33688=ORIENTED_EDGE ( 'NONE', *, *, #22078, .T. ) ;
#33720=CIRCLE ( 'NONE', #28673, 2.000000000000000444 ) ;
#33737=EDGE_LOOP ( 'NONE', ( #19639, #19227, #16884, #34803, #6942 ) ) ;
#33739=DIRECTION ( 'NONE',  ( 0.000000000000000000, -0.9242245927363028635, -0.3818493186865930533 ) ) ;
#33742=DIRECTION ( 'NONE',  ( 1.000000000000000000, 0.000000000000000000, -0.000000000000000000 ) ) ;
#33758=ORIENTED_EDGE ( 'NONE', *, *, #41864, .F. ) ;
#33760=AXIS2_PLACEMENT_3D ( 'NONE', #36302, #39517, #39288 ) ;
#33772=CARTESIAN_POINT ( 'NONE',  ( 85.04324155394569118, -27.84333996136784961, -14.15691383771150136 ) ) ;
#33781=ORIENTED_EDGE ( 'NONE', *, *, #15292, .T. ) ;
#33820=EDGE_CURVE ( 'NONE', #26936, #11048, #25384, .T. ) ;
#33826=ORIENTED_EDGE ( 'NONE', *, *, #24355, .F. ) ;
#33836=LINE ( 'NONE', #34293, #29490 ) ;
#33854=DIRECTION ( 'NONE',  ( -0.8949343913984424415, -0.4123869368673878655, -0.1703803081152052423 ) ) ;
#33866=AXIS2_PLACEMENT_3D ( 'NONE', #19372, #5006, #12317 ) ;
#33903=DIRECTION ( 'NONE',  ( -1.224775218828351862E-16, 0.3818493186865896671, -0.9242245927363043068 ) ) ;
#33910=CARTESIAN_POINT ( 'NONE',  ( 94.20708369096698220, -24.88943055980569241, -13.49371108670732333 ) ) ;
#33912=CARTESIAN_POINT ( 'NONE',  ( 90.33554924625337890, -25.99489077589524300, -13.39321520033831447 ) ) ;
#33915=ORIENTED_EDGE ( 'NONE', *, *, #15579, .T. ) ;
#33928=ADVANCED_FACE ( 'NONE', ( #7437 ), #27991, .T. ) ;
#33933=ORIENTED_EDGE ( 'NONE', *, *, #31970, .F. ) ;
#33941=DIRECTION ( 'NONE',  ( 0.000000000000000000, -0.9242245927363034186, -0.3818493186865916655 ) ) ;
#33943=ADVANCED_FACE ( 'NONE', ( #11103 ), #17986, .F. ) ;
#33944=CARTESIAN_POINT ( 'NONE',  ( 121.9470836909669913, -24.14644159042263993, -12.62951656296512937 ) ) ;
#33960=ORIENTED_EDGE ( 'NONE', *, *, #37536, .F. ) ;
#33972=DIRECTION ( 'NONE',  ( 0.000000000000000000, -0.9242245927363028635, -0.3818493186865927758 ) ) ;
#34045=AXIS2_PLACEMENT_3D ( 'NONE', #366, #18147, #21791 ) ;
#34051=DIRECTION ( 'NONE',  ( 0.000000000000000000, -0.3818493186865936084, 0.9242245927363024194 ) ) ;
#34069=CYLINDRICAL_SURFACE ( 'NONE', #23715, 4.000000000000000888 ) ;
#34079=DIRECTION ( 'NONE',  ( 1.000000000000000000, 0.000000000000000000, -0.000000000000000000 ) ) ;
#34104=ORIENTED_EDGE ( 'NONE', *, *, #37844, .F. ) ;
#34128=ORIENTED_EDGE ( 'NONE', *, *, #30077, .F. ) ;
#34139=DIRECTION ( 'NONE',  ( 1.000000000000000000, 0.000000000000000000, -0.000000000000000000 ) ) ;
#34153=AXIS2_PLACEMENT_3D ( 'NONE', #7448, #17950, #10671 ) ;
#34204=ADVANCED_FACE ( 'NONE', ( #26357 ), #28186, .T. ) ;
#34205=CARTESIAN_POINT ( 'NONE',  ( 94.86797725101170897, -25.23805398138116018, -13.87635650542741850 ) ) ;
#34209=EDGE_CURVE ( 'NONE', #29406, #13605, #4868, .T. ) ;
#34212=AXIS2_PLACEMENT_3D ( 'NONE', #30783, #41064, #12562 ) ;
#34230=ADVANCED_FACE ( 'NONE', ( #4918 ), #40560, .T. ) ;
#34241=EDGE_CURVE ( 'NONE', #31913, #13199, #9971, .T. ) ;
#34246=AXIS2_PLACEMENT_3D ( 'NONE', #30731, #33229, #36653 ) ;
#34252=DIRECTION ( 'NONE',  ( 0.000000000000000000, 0.9242245927363040847, 0.3818493186865897226 ) ) ;
#34269=ORIENTED_EDGE ( 'NONE', *, *, #20054, .T. ) ;
#34273=CARTESIAN_POINT ( 'NONE',  ( 96.54708369096698561, -27.78532125115470208, -14.69016690077367926 ) ) ;
#34287=AXIS2_PLACEMENT_3D ( 'NONE', #40447, #8, #10504 ) ;
#34293=CARTESIAN_POINT ( 'NONE',  ( 96.54708369096698561, -28.17862604940189541, -13.73821557025528683 ) ) ;
#34320=ORIENTED_EDGE ( 'NONE', *, *, #20879, .T. ) ;
#34323=AXIS2_PLACEMENT_3D ( 'NONE', #5983, #17171, #31060 ) ;
#34337=CARTESIAN_POINT ( 'NONE',  ( 88.07785292173620917, -25.99489077589524300, -13.39321520033831625 ) ) ;
#34342=CARTESIAN_POINT ( 'NONE',  ( 95.62170725701128049, -26.77595362744983376, -12.85143736872905507 ) ) ;
#34351=DIRECTION ( 'NONE',  ( 0.000000000000000000, -0.3818493186865936084, 0.9242245927363024194 ) ) ;
#34366=DIRECTION ( 'NONE',  ( 0.000000000000000000, -0.3818493186865927203, 0.9242245927363029745 ) ) ;
#34389=FACE_OUTER_BOUND ( 'NONE', #16631, .T. ) ;
#34395=CIRCLE ( 'NONE', #4527, 6.500000000000000000 ) ;
#34406=AXIS2_PLACEMENT_3D ( 'NONE', #33592, #19262, #26327 ) ;
#34424=CARTESIAN_POINT ( 'NONE',  ( 94.20708369096698220, -25.26022072204669655, -13.82270432939535709 ) ) ;
#34447=CARTESIAN_POINT ( 'NONE',  ( 87.14323352029596492, -26.75858941326842810, -11.54476601486570964 ) ) ;
#34454=ORIENTED_EDGE ( 'NONE', *, *, #41214, .T. ) ;
#34456=CIRCLE ( 'NONE', #35922, 1.610000000000000986 ) ;
#34500=LINE ( 'NONE', #23828, #9158 ) ;
#34509=EDGE_CURVE ( 'NONE', #43753, #39217, #13803, .T. ) ;
#34515=DIRECTION ( 'NONE',  ( 1.000000000000000000, 0.000000000000000000, -0.000000000000000000 ) ) ;
#34517=ORIENTED_EDGE ( 'NONE', *, *, #40661, .F. ) ;
#34524=CARTESIAN_POINT ( 'NONE',  ( 94.86797725101156686, -25.79977623989092805, -12.51676909700203666 ) ) ;
#34542=VERTEX_POINT ( 'NONE', #5816 ) ;
#34553=DIRECTION ( 'NONE',  ( 1.000000000000000000, 0.000000000000000000, -0.000000000000000000 ) ) ;
#34567=ORIENTED_EDGE ( 'NONE', *, *, #17775, .T. ) ;
#34568=DIRECTION ( 'NONE',  ( 1.000000000000000000, 0.000000000000000000, -0.000000000000000000 ) ) ;
#34577=CIRCLE ( 'NONE', #10584, 1.610000000000000986 ) ;
#34587=ORIENTED_EDGE ( 'NONE', *, *, #28832, .F. ) ;
#34603=EDGE_CURVE ( 'NONE', #28337, #22202, #9941, .T. ) ;
#34609=CARTESIAN_POINT ( 'NONE',  ( 84.38170309240724976, -24.14644159042263993, -12.62951656296512937 ) ) ;
#34615=EDGE_CURVE ( 'NONE', #13545, #36181, #6351, .T. ) ;
#34634=DIRECTION ( 'NONE',  ( 1.000000000000000000, 0.000000000000000000, -0.000000000000000000 ) ) ;
#34645=LINE ( 'NONE', #20766, #35927 ) ;
#34650=VECTOR ( 'NONE', #12301, 1000.000000000000227 ) ;
#34660=ORIENTED_EDGE ( 'NONE', *, *, #22277, .F. ) ;
#34664=DIRECTION ( 'NONE',  ( 0.000000000000000000, -0.3818493186865936084, 0.9242245927363024194 ) ) ;
#34705=DIRECTION ( 'NONE',  ( 0.5735764363510498232, -0.3127926500124802445, 0.7570804645221007600 ) ) ;
#34708=CARTESIAN_POINT ( 'NONE',  ( 89.12784890491134604, -25.99489077589524300, -13.39321520033831625 ) ) ;
#34710=ORIENTED_EDGE ( 'NONE', *, *, #13608, .F. ) ;
#34721=DIRECTION ( 'NONE',  ( 1.000000000000000000, 0.000000000000000000, -0.000000000000000000 ) ) ;
#34726=DIRECTION ( 'NONE',  ( 0.5735764363510498232, -0.3127926500124802445, 0.7570804645221007600 ) ) ;
#34728=EDGE_CURVE ( 'NONE', #8919, #22099, #16503, .T. ) ;
#34761=EDGE_CURVE ( 'NONE', #2194, #20823, #39080, .T. ) ;
#34763=EDGE_CURVE ( 'NONE', #8410, #31533, #19421, .T. ) ;
#34803=ORIENTED_EDGE ( 'NONE', *, *, #42588, .T. ) ;
#34833=DIRECTION ( 'NONE',  ( 0.000000000000000000, -0.9242245927363028635, -0.3818493186865927758 ) ) ;
#34838=CARTESIAN_POINT ( 'NONE',  ( 87.80477198183443477, -26.75858941326842810, -11.54476601486570964 ) ) ;
#34871=ORIENTED_EDGE ( 'NONE', *, *, #27901, .F. ) ;
#34875=CIRCLE ( 'NONE', #18889, 2.000000000000000444 ) ;
#34905=FACE_OUTER_BOUND ( 'NONE', #24473, .T. ) ;
#34908=TOROIDAL_SURFACE ( 'NONE', #15273, 2.200000000000000178, 0.2000000000000000111 ) ;
#34966=ORIENTED_EDGE ( 'NONE', *, *, #35754, .F. ) ;
#34978=CIRCLE ( 'NONE', #16841, 2.000000000000000444 ) ;
#34990=AXIS2_PLACEMENT_3D ( 'NONE', #5195, #2001, #22983 ) ;
#35029=AXIS2_PLACEMENT_3D ( 'NONE', #9827, #33742, #33972 ) ;
#35031=CARTESIAN_POINT ( 'NONE',  ( 89.01247232317646763, -25.23119213852205789, -15.24166438581092109 ) ) ;
#35032=ORIENTED_EDGE ( 'NONE', *, *, #43690, .F. ) ;
#35056=EDGE_CURVE ( 'NONE', #5805, #31941, #5610, .T. ) ;
#35058=VERTEX_POINT ( 'NONE', #37541 ) ;
#35062=DIRECTION ( 'NONE',  ( 0.000000000000000000, -0.3818493186865927203, 0.9242245927363029745 ) ) ;
#35073=DIRECTION ( 'NONE',  ( 1.000000000000000000, 0.000000000000000000, -0.000000000000000000 ) ) ;
#35074=EDGE_LOOP ( 'NONE', ( #18226, #34128, #31528, #29915, #35407 ) ) ;
#35085=CARTESIAN_POINT ( 'NONE',  ( 93.93057702947278642, -25.99489077589524300, -13.39321520033831447 ) ) ;
#35094=AXIS2_PLACEMENT_3D ( 'NONE', #18948, #16614, #27096 ) ;
#35098=CIRCLE ( 'NONE', #35827, 1.009117809157100254 ) ;
#35105=EDGE_CURVE ( 'NONE', #16022, #30207, #22732, .T. ) ;
#35137=AXIS2_PLACEMENT_3D ( 'NONE', #42512, #1000, #28156 ) ;
#35146=VERTEX_POINT ( 'NONE', #19322 ) ;
#35149=CARTESIAN_POINT ( 'NONE',  ( 88.07785292173620917, -26.60966817898065884, -11.90521360603286816 ) ) ;
#35153=CARTESIAN_POINT ( 'NONE',  ( 87.41631446019775353, -25.38011337280982715, -14.88121679464376257 ) ) ;
#35166=AXIS2_PLACEMENT_3D ( 'NONE', #40666, #9418, #44321 ) ;
#35171=VERTEX_POINT ( 'NONE', #22962 ) ;
#35176=EDGE_CURVE ( 'NONE', #5526, #23066, #7807, .T. ) ;
#35178=EDGE_LOOP ( 'NONE', ( #15988, #32955, #3726, #37445 ) ) ;
#35185=FACE_OUTER_BOUND ( 'NONE', #33566, .T. ) ;
#35189=CARTESIAN_POINT ( 'NONE',  ( 96.54708369096698561, -27.78532125115470208, -14.69016690077367926 ) ) ;
#35203=CONICAL_SURFACE ( 'NONE', #39585, 2.000000000000000444, 0.9599310885968830309 ) ;
#35205=CIRCLE ( 'NONE', #19830, 2.000000000000000444 ) ;
#35212=CIRCLE ( 'NONE', #31582, 2.000000000000000444 ) ;
#35251=DIRECTION ( 'NONE',  ( 0.000000000000000000, -0.9242245927363029745, -0.3818493186865927758 ) ) ;
#35264=ADVANCED_FACE ( 'NONE', ( #5850 ), #26161, .T. ) ;
#35286=ORIENTED_EDGE ( 'NONE', *, *, #13645, .T. ) ;
#35290=CARTESIAN_POINT ( 'NONE',  ( 121.9470836909669913, -24.14644159042263993, -12.62951656296512937 ) ) ;
#35313=CARTESIAN_POINT ( 'NONE',  ( 91.11246428952674137, -26.75858941326842810, -11.54476601486570964 ) ) ;
#35321=EDGE_CURVE ( 'NONE', #38363, #8497, #43703, .T. ) ;
#35326=VECTOR ( 'NONE', #34705, 1000.000000000000114 ) ;
#35332=DIRECTION ( 'NONE',  ( 1.000000000000000000, 0.000000000000000000, -0.000000000000000000 ) ) ;
#35343=ORIENTED_EDGE ( 'NONE', *, *, #41310, .T. ) ;
#35358=DIRECTION ( 'NONE',  ( 0.000000000000000000, -0.9242245927363028635, -0.3818493186865930533 ) ) ;
#35361=EDGE_CURVE ( 'NONE', #30793, #38132, #10418, .T. ) ;
#35374=AXIS2_PLACEMENT_3D ( 'NONE', #22427, #16274, #5992 ) ;
#35375=CARTESIAN_POINT ( 'NONE',  ( 95.62170725701133733, -25.05980814603879026, -13.56410367930211969 ) ) ;
#35405=AXIS2_PLACEMENT_3D ( 'NONE', #34708, #41815, #31967 ) ;
#35407=ORIENTED_EDGE ( 'NONE', *, *, #39042, .T. ) ;
#35414=DIRECTION ( 'NONE',  ( 0.000000000000000000, -0.9242245927363028635, -0.3818493186865930533 ) ) ;
#35416=AXIS2_PLACEMENT_3D ( 'NONE', #36373, #25906, #12683 ) ;
#35430=VERTEX_POINT ( 'NONE', #30262 ) ;
#35431=AXIS2_PLACEMENT_3D ( 'NONE', #13220, #27119, #20282 ) ;
#35442=CARTESIAN_POINT ( 'NONE',  ( 90.04708369096697140, -25.51891511063604767, -13.19656280121471958 ) ) ;
#35444=VECTOR ( 'NONE', #9510, 1000.000000000000000 ) ;
#35467=CARTESIAN_POINT ( 'NONE',  ( 96.21525317080913453, -25.71306530104311605, -15.42404253659028335 ) ) ;
#35494=CARTESIAN_POINT ( 'NONE',  ( 121.9470836909669913, -27.84333996136784961, -14.15691383771150136 ) ) ;
#35508=DIRECTION ( 'NONE',  ( 0.000000000000000000, -0.3818493186865927203, 0.9242245927363029745 ) ) ;
#35532=ORIENTED_EDGE ( 'NONE', *, *, #39875, .F. ) ;
#35544=CARTESIAN_POINT ( 'NONE',  ( 84.49707967414211396, -26.75858941326842810, -11.54476601486570964 ) ) ;
#35550=EDGE_LOOP ( 'NONE', ( #41647, #33688, #7461, #5721, #39619, #32748 ) ) ;
#35557=DIRECTION ( 'NONE',  ( 0.000000000000000000, -0.3818493186865927203, 0.9242245927363029745 ) ) ;
#35564=DIRECTION ( 'NONE',  ( -0.4461977533474357771, -0.3417300876246960328, 0.8271203734159368048 ) ) ;
#35574=DIRECTION ( 'NONE',  ( 0.000000000000000000, 0.3818493186865927203, -0.9242245927363029745 ) ) ;
#35575=DIRECTION ( 'NONE',  ( 1.000000000000000000, 0.000000000000000000, -0.000000000000000000 ) ) ;
#35587=EDGE_CURVE ( 'NONE', #21924, #19363, #3252, .T. ) ;
#35594=CARTESIAN_POINT ( 'NONE',  ( 90.48265143217095385, -26.80230621008286107, -13.72680406592863456 ) ) ;
#35607=CIRCLE ( 'NONE', #41474, 2.000000000000000444 ) ;
#35621=CARTESIAN_POINT ( 'NONE',  ( 85.15861813568058380, -24.14644159042263993, -12.62951656296512937 ) ) ;
#35629=VERTEX_POINT ( 'NONE', #41444 ) ;
#35631=DIRECTION ( 'NONE',  ( 1.000000000000000000, 0.000000000000000000, -0.000000000000000000 ) ) ;
#35637=EDGE_CURVE ( 'NONE', #40373, #44289, #10202, .T. ) ;
#35643=ADVANCED_FACE ( 'NONE', ( #6778 ), #22187, .T. ) ;
#35658=CARTESIAN_POINT ( 'NONE',  ( 88.07785292173620917, -26.60966817898065884, -11.90521360603286816 ) ) ;
#35662=ORIENTED_EDGE ( 'NONE', *, *, #15439, .F. ) ;
#35664=CARTESIAN_POINT ( 'NONE',  ( 89.12784890491134604, -25.99489077589524300, -13.39321520033831625 ) ) ;
#35667=ORIENTED_EDGE ( 'NONE', *, *, #38421, .F. ) ;
#35673=DIRECTION ( 'NONE',  ( 0.000000000000000000, -0.3818493186865927203, 0.9242245927363029745 ) ) ;
#35685=DIRECTION ( 'NONE',  ( 1.000000000000000000, 0.000000000000000000, -0.000000000000000000 ) ) ;
#35690=ORIENTED_EDGE ( 'NONE', *, *, #13042, .T. ) ;
#35696=CARTESIAN_POINT ( 'NONE',  ( 95.62170725701142260, -26.16577925485904288, -14.32829783019477432 ) ) ;
#35701=AXIS2_PLACEMENT_3D ( 'NONE', #40320, #26861, #12512 ) ;
#35725=EDGE_LOOP ( 'NONE', ( #17065, #15263, #5002, #33519, #18047 ) ) ;
#35731=AXIS2_PLACEMENT_3D ( 'NONE', #20746, #17328, #17543 ) ;
#35753=CARTESIAN_POINT ( 'NONE',  ( 91.38554522942851577, -26.60966817898065884, -11.90521360603286816 ) ) ;
#35754=EDGE_CURVE ( 'NONE', #35430, #24400, #2150, .T. ) ;
#35792=DIRECTION ( 'NONE',  ( -0.5735764363510450492, -0.3127926500124816878, 0.7570804645221038687 ) ) ;
#35802=CARTESIAN_POINT ( 'NONE',  ( 91.65862616933031859, -27.84333996136784961, -14.15691383771150136 ) ) ;
#35813=DIRECTION ( 'NONE',  ( 1.000000000000000000, 0.000000000000000000, -0.000000000000000000 ) ) ;
#35815=DIRECTION ( 'NONE',  ( 1.000000000000000000, 0.000000000000000000, -0.000000000000000000 ) ) ;
#35827=AXIS2_PLACEMENT_3D ( 'NONE', #4797, #35575, #4121 ) ;
#35836=CIRCLE ( 'NONE', #890, 1.610000000000000986 ) ;
#35837=ORIENTED_EDGE ( 'NONE', *, *, #11933, .T. ) ;
#35841=EDGE_CURVE ( 'NONE', #37865, #33593, #41503, .T. ) ;
#35857=VERTEX_POINT ( 'NONE', #40251 ) ;
#35875=DIRECTION ( 'NONE',  ( 0.000000000000000000, -0.9242245927363028635, -0.3818493186865930533 ) ) ;
#35881=ORIENTED_EDGE ( 'NONE', *, *, #44846, .T. ) ;
#35891=CIRCLE ( 'NONE', #19900, 2.000000000000000444 ) ;
#35910=CARTESIAN_POINT ( 'NONE',  ( 87.41631446019775353, -25.99489077589524300, -13.39321520033831625 ) ) ;
#35911=FACE_OUTER_BOUND ( 'NONE', #24021, .T. ) ;
#35917=DIRECTION ( 'NONE',  ( 0.5735764363510499342, 0.3127926500124801890, -0.7570804645221008711 ) ) ;
#35922=AXIS2_PLACEMENT_3D ( 'NONE', #1509, #439, #10938 ) ;
#35927=VECTOR ( 'NONE', #10285, 1000.000000000000114 ) ;
#35952=EDGE_CURVE ( 'NONE', #41727, #1522, #14903, .T. ) ;
#35973=VERTEX_POINT ( 'NONE', #7931 ) ;
#36002=ORIENTED_EDGE ( 'NONE', *, *, #30360, .T. ) ;
#36070=ORIENTED_EDGE ( 'NONE', *, *, #35952, .T. ) ;
#36097=ORIENTED_EDGE ( 'NONE', *, *, #36154, .F. ) ;
#36124=LINE ( 'NONE', #4893, #3318 ) ;
#36144=CIRCLE ( 'NONE', #7778, 1.610000000000000986 ) ;
#36154=EDGE_CURVE ( 'NONE', #37642, #10139, #24923, .T. ) ;
#36162=LINE ( 'NONE', #25916, #27950 ) ;
#36163=ORIENTED_EDGE ( 'NONE', *, *, #6936, .T. ) ;
#36171=AXIS2_PLACEMENT_3D ( 'NONE', #44325, #26532, #40442 ) ;
#36175=FACE_OUTER_BOUND ( 'NONE', #21964, .T. ) ;
#36180=EDGE_CURVE ( 'NONE', #14958, #20548, #29243, .T. ) ;
#36181=VERTEX_POINT ( 'NONE', #32866 ) ;
#36189=MANIFOLD_SOLID_BREP ( 'NONE', #39616 ) ;
#36190=DIRECTION ( 'NONE',  ( 1.000000000000000000, 0.000000000000000000, -0.000000000000000000 ) ) ;
#36206=DIRECTION ( 'NONE',  ( 1.000000000000000000, 0.000000000000000000, -0.000000000000000000 ) ) ;
#36214=ADVANCED_FACE ( 'NONE', ( #12828 ), #2087, .T. ) ;
#36218=EDGE_LOOP ( 'NONE', ( #17035, #29108, #12674, #37661, #25182 ) ) ;
#36223=CARTESIAN_POINT ( 'NONE',  ( 96.46827370896536991, -25.99489077589524300, -13.39321520033831447 ) ) ;
#36236=ORIENTED_EDGE ( 'NONE', *, *, #20863, .T. ) ;
#36243=CARTESIAN_POINT ( 'NONE',  ( 96.54708369096698561, -27.29184247633061489, -11.60278472507885894 ) ) ;
#36294=ORIENTED_EDGE ( 'NONE', *, *, #31968, .T. ) ;
#36302=CARTESIAN_POINT ( 'NONE',  ( 85.04324155394569118, -25.99489077589524300, -13.39321520033831447 ) ) ;
#36335=EDGE_LOOP ( 'NONE', ( #45026, #39948, #21305, #14875, #18977, #7522 ) ) ;
#36344=AXIS2_PLACEMENT_3D ( 'NONE', #13586, #11056, #25190 ) ;
#36351=VERTEX_POINT ( 'NONE', #8946 ) ;
#36373=CARTESIAN_POINT ( 'NONE',  ( 87.80477198183443477, -25.99489077589524300, -13.39321520033831625 ) ) ;
#36395=DIRECTION ( 'NONE',  ( 1.000000000000000000, 0.000000000000000000, -0.000000000000000000 ) ) ;
#36398=FACE_OUTER_BOUND ( 'NONE', #38847, .T. ) ;
#36400=PLANE ( 'NONE',  #39315 ) ;
#36426=CARTESIAN_POINT ( 'NONE',  ( 87.41631446019775353, -25.99489077589524300, -13.39321520033831625 ) ) ;
#36436=CARTESIAN_POINT ( 'NONE',  ( 93.44708369096697709, -29.69178914684045623, -14.92061247508468647 ) ) ;
#36439=VERTEX_POINT ( 'NONE', #33772 ) ;
#36446=EDGE_CURVE ( 'NONE', #24723, #2587, #34577, .T. ) ;
#36452=CARTESIAN_POINT ( 'NONE',  ( 90.99708770779186295, -26.75858941326842810, -11.54476601486570964 ) ) ;
#36459=EDGE_LOOP ( 'NONE', ( #41302, #8317, #41652, #489, #18248, #8264 ) ) ;
#36462=LINE ( 'NONE', #5232, #10228 ) ;
#36463=AXIS2_PLACEMENT_3D ( 'NONE', #12772, #5236, #32815 ) ;
#36484=CIRCLE ( 'NONE', #16859, 1.610000000000000986 ) ;
#36515=VERTEX_POINT ( 'NONE', #23768 ) ;
#36516=AXIS2_PLACEMENT_3D ( 'NONE', #44480, #34634, #3420 ) ;
#36583=DIRECTION ( 'NONE',  ( 1.000000000000000000, 0.000000000000000000, -0.000000000000000000 ) ) ;
#36584=AXIS2_PLACEMENT_3D ( 'NONE', #43770, #44229, #12536 ) ;
#36587=CARTESIAN_POINT ( 'NONE',  ( 95.62170725701133733, -26.53666860750450951, -14.17427805189290346 ) ) ;
#36598=LINE ( 'NONE', #44147, #4037 ) ;
#36603=DIRECTION ( 'NONE',  ( 0.000000000000000000, -0.3818493186865936084, 0.9242245927363024194 ) ) ;
#36611=CARTESIAN_POINT ( 'NONE',  ( 90.04708369096697140, -25.51891511063604767, -13.19656280121471958 ) ) ;
#36622=CARTESIAN_POINT ( 'NONE',  ( 92.04708369096698561, -25.99489077589524300, -13.39321520033831625 ) ) ;
#36632=CARTESIAN_POINT ( 'NONE',  ( 121.9470836909669913, -25.99489077589524300, -13.39321520033831447 ) ) ;
#36651=CARTESIAN_POINT ( 'NONE',  ( 83.83554121260367253, -25.99489077589524300, -13.39321520033831625 ) ) ;
#36653=DIRECTION ( 'NONE',  ( 0.000000000000000000, -0.3818493186865936084, 0.9242245927363024194 ) ) ;
#36659=CARTESIAN_POINT ( 'NONE',  ( 94.20708369096698220, -26.21217205256509075, -14.21600912764254687 ) ) ;
#36665=FILL_AREA_STYLE_COLOUR ( '', #43089 ) ;
#36668=LINE ( 'NONE', #22769, #34650 ) ;
#36707=DIRECTION ( 'NONE',  ( 1.000000000000000000, 0.000000000000000000, -0.000000000000000000 ) ) ;
#36722=ORIENTED_EDGE ( 'NONE', *, *, #39569, .F. ) ;
#36723=EDGE_CURVE ( 'NONE', #35430, #37642, #33102, .T. ) ;
#36726=CARTESIAN_POINT ( 'NONE',  ( 94.20708369096698220, -25.26022072204669655, -13.82270432939535709 ) ) ;
#36760=LINE ( 'NONE', #18779, #9427 ) ;
#36784=EDGE_LOOP ( 'NONE', ( #10845, #14062, #26367, #13994, #33446 ) ) ;
#36785=EDGE_CURVE ( 'NONE', #37027, #21347, #8392, .T. ) ;
#36805=CARTESIAN_POINT ( 'NONE',  ( 93.24708369096698846, -28.02818487991510921, -14.23328370144882093 ) ) ;
#36808=DIRECTION ( 'NONE',  ( 0.5735764363510499342, 0.3127926500124801890, -0.7570804645221008711 ) ) ;
#36811=ORIENTED_EDGE ( 'NONE', *, *, #36180, .F. ) ;
#36820=DIRECTION ( 'NONE',  ( 0.000000000000000000, -0.3818493186865927203, 0.9242245927363029745 ) ) ;
#36833=CIRCLE ( 'NONE', #27390, 2.000000000000000444 ) ;
#36845=VECTOR ( 'NONE', #23334, 1000.000000000000000 ) ;
#36854=CARTESIAN_POINT ( 'NONE',  ( 88.35093386163799778, -25.99489077589524300, -13.39321520033831447 ) ) ;
#36858=DIRECTION ( 'NONE',  ( 0.000000000000000000, -0.3818493186865936084, 0.9242245927363024194 ) ) ;
#36876=CIRCLE ( 'NONE', #39069, 2.000000000000000444 ) ;
#36878=ORIENTED_EDGE ( 'NONE', *, *, #41778, .T. ) ;
#36897=FACE_OUTER_BOUND ( 'NONE', #40166, .T. ) ;
#36905=DIRECTION ( 'NONE',  ( 0.000000000000000000, -0.3818493186865927203, 0.9242245927363029745 ) ) ;
#36920=ORIENTED_EDGE ( 'NONE', *, *, #7463, .F. ) ;
#36979=ORIENTED_EDGE ( 'NONE', *, *, #25420, .F. ) ;
#36988=ORIENTED_EDGE ( 'NONE', *, *, #6923, .F. ) ;
#36999=ORIENTED_EDGE ( 'NONE', *, *, #24038, .T. ) ;
#37008=EDGE_CURVE ( 'NONE', #7716, #16407, #27317, .T. ) ;
#37015=DIRECTION ( 'NONE',  ( 1.000000000000000000, 0.000000000000000000, -0.000000000000000000 ) ) ;
#37027=VERTEX_POINT ( 'NONE', #6375 ) ;
#37070=EDGE_CURVE ( 'NONE', #42191, #41162, #27121, .T. ) ;
#37076=DIRECTION ( 'NONE',  ( 0.000000000000000000, -0.3818493186865927203, 0.9242245927363029745 ) ) ;
#37078=DIRECTION ( 'NONE',  ( 1.000000000000000000, 0.000000000000000000, -0.000000000000000000 ) ) ;
#37120=CARTESIAN_POINT ( 'NONE',  ( 88.46631044337289040, -26.75858941326842810, -11.54476601486570964 ) ) ;
#37128=CIRCLE ( 'NONE', #8731, 2.000000000000000444 ) ;
#37135=DIRECTION ( 'NONE',  ( 1.000000000000000000, 0.000000000000000000, -0.000000000000000000 ) ) ;
#37160=VERTEX_POINT ( 'NONE', #24157 ) ;
#37190=CONICAL_SURFACE ( 'NONE', #32830, 2.000000000000000444, 0.9599310885968830309 ) ;
#37202=AXIS2_PLACEMENT_3D ( 'NONE', #4648, #15149, #15596 ) ;
#37207=ORIENTED_EDGE ( 'NONE', *, *, #1356, .T. ) ;
#37220=DIRECTION ( 'NONE',  ( 0.000000000000000000, -0.3818493186865927203, 0.9242245927363029745 ) ) ;
#37237=CIRCLE ( 'NONE', #40159, 2.000000000000000444 ) ;
#37275=CARTESIAN_POINT ( 'NONE',  ( 85.15861813568058380, -25.99489077589524300, -13.39321520033831625 ) ) ;
#37309=DIRECTION ( 'NONE',  ( 1.000000000000000000, 0.000000000000000000, -0.000000000000000000 ) ) ;
#37326=VECTOR ( 'NONE', #16907, 1000.000000000000000 ) ;
#37367=DIRECTION ( 'NONE',  ( 0.000000000000000000, 0.3818493186865928868, -0.9242245927363029745 ) ) ;
#37387=CARTESIAN_POINT ( 'NONE',  ( 89.40092984481313465, -25.38011337280982715, -14.88121679464376257 ) ) ;
#37388=CARTESIAN_POINT ( 'NONE',  ( 84.10862215250544693, -25.38011337280982715, -14.88121679464376257 ) ) ;
#37408=FACE_OUTER_BOUND ( 'NONE', #18974, .T. ) ;
#37445=ORIENTED_EDGE ( 'NONE', *, *, #42473, .F. ) ;
#37473=ORIENTED_EDGE ( 'NONE', *, *, #44180, .T. ) ;
#37492=AXIS2_PLACEMENT_3D ( 'NONE', #27071, #30937, #10198 ) ;
#37532=DIRECTION ( 'NONE',  ( 0.000000000000000000, -0.9242245927363029745, -0.3818493186865927758 ) ) ;
#37536=EDGE_CURVE ( 'NONE', #8271, #11048, #18612, .T. ) ;
#37541=CARTESIAN_POINT ( 'NONE',  ( 90.06246830635160450, -26.60966817898065884, -11.90521360603286816 ) ) ;
#37568=CARTESIAN_POINT ( 'NONE',  ( 84.38170309240724976, -25.99489077589524300, -13.39321520033831447 ) ) ;
#37578=CARTESIAN_POINT ( 'NONE',  ( 84.77016061404391678, -25.38011337280982715, -14.88121679464376257 ) ) ;
#37617=DIRECTION ( 'NONE',  ( 0.000000000000000000, -0.9242245927363029745, -0.3818493186865927203 ) ) ;
#37624=ORIENTED_EDGE ( 'NONE', *, *, #32712, .F. ) ;
#37629=CONICAL_SURFACE ( 'NONE', #39805, 1.610000000000000986, 0.9599310885968765916 ) ;
#37642=VERTEX_POINT ( 'NONE', #10195 ) ;
#37644=AXIS2_PLACEMENT_3D ( 'NONE', #27059, #40979, #37532 ) ;
#37647=ORIENTED_EDGE ( 'NONE', *, *, #44819, .T. ) ;
#37655=ORIENTED_EDGE ( 'NONE', *, *, #44274, .T. ) ;
#37661=ORIENTED_EDGE ( 'NONE', *, *, #11932, .T. ) ;
#37670=EDGE_LOOP ( 'NONE', ( #32243, #39989, #33349, #3480, #16920 ) ) ;
#37690=ORIENTED_EDGE ( 'NONE', *, *, #15719, .F. ) ;
#37701=CIRCLE ( 'NONE', #27515, 1.610000000000000986 ) ;
#37705=CARTESIAN_POINT ( 'NONE',  ( 121.9470836909669913, -25.99489077589524300, -13.39321520033831447 ) ) ;
#37715=FACE_OUTER_BOUND ( 'NONE', #16007, .T. ) ;
#37727=DIRECTION ( 'NONE',  ( 0.000000000000000000, -0.3818493186865927203, 0.9242245927363029745 ) ) ;
#37744=DIRECTION ( 'NONE',  ( 1.000000000000000000, 0.000000000000000000, -0.000000000000000000 ) ) ;
#37751=ORIENTED_EDGE ( 'NONE', *, *, #36723, .F. ) ;
#37760=CARTESIAN_POINT ( 'NONE',  ( 90.33554924625337890, -25.99489077589524300, -13.39321520033831447 ) ) ;
#37778=DIRECTION ( 'NONE',  ( 0.000000000000000000, -0.3818493186865927203, 0.9242245927363029745 ) ) ;
#37780=FACE_OUTER_BOUND ( 'NONE', #7868, .T. ) ;
#37792=CARTESIAN_POINT ( 'NONE',  ( 94.20708369096698220, -25.14343533174585943, -14.10537061818067883 ) ) ;
#37813=CARTESIAN_POINT ( 'NONE',  ( 121.9470836909669913, -27.84333996136784961, -14.15691383771150136 ) ) ;
#37823=CONICAL_SURFACE ( 'NONE', #7257, 2.000000000000000444, 0.9599310885968830309 ) ;
#37828=AXIS2_PLACEMENT_3D ( 'NONE', #31660, #28258, #29600 ) ;
#37832=ORIENTED_EDGE ( 'NONE', *, *, #6805, .F. ) ;
#37835=EDGE_CURVE ( 'NONE', #21444, #23574, #138, .T. ) ;
#37844=EDGE_CURVE ( 'NONE', #7733, #14619, #38642, .T. ) ;
#37861=EDGE_CURVE ( 'NONE', #2441, #25522, #31813, .T. ) ;
#37865=VERTEX_POINT ( 'NONE', #27968 ) ;
#37931=AXIS2_PLACEMENT_3D ( 'NONE', #38274, #11153, #14119 ) ;
#37934=EDGE_CURVE ( 'NONE', #24250, #20548, #36124, .T. ) ;
#37935=CARTESIAN_POINT ( 'NONE',  ( 84.77016061404391678, -25.99489077589524300, -13.39321520033831625 ) ) ;
#37938=DIRECTION ( 'NONE',  ( 1.000000000000000000, 0.000000000000000000, -0.000000000000000000 ) ) ;
#37948=DIRECTION ( 'NONE',  ( 1.000000000000000000, 0.000000000000000000, -0.000000000000000000 ) ) ;
#37950=FACE_OUTER_BOUND ( 'NONE', #43378, .T. ) ;
#37953=DIRECTION ( 'NONE',  ( 0.5735764363510498232, -0.3127926500124802445, 0.7570804645221007600 ) ) ;
#37955=EDGE_LOOP ( 'NONE', ( #12190, #29227, #38757, #43745, #41465 ) ) ;
#37968=DIRECTION ( 'NONE',  ( 0.000000000000000000, -0.3818493186865927203, 0.9242245927363029745 ) ) ;
#37982=ORIENTED_EDGE ( 'NONE', *, *, #3000, .F. ) ;
#37993=VECTOR ( 'NONE', #18238, 1000.000000000000000 ) ;
#38003=EDGE_CURVE ( 'NONE', #5526, #20846, #40008, .T. ) ;
#38020=DIRECTION ( 'NONE',  ( 1.000000000000000000, 0.000000000000000000, -0.000000000000000000 ) ) ;
#38031=CARTESIAN_POINT ( 'NONE',  ( 91.77400275106518279, -24.14644159042263993, -12.62951656296512937 ) ) ;
#38038=CARTESIAN_POINT ( 'NONE',  ( 94.20708369096698220, -25.99489077589524300, -13.39321520033831447 ) ) ;
#38063=AXIS2_PLACEMENT_3D ( 'NONE', #29519, #37015, #15844 ) ;
#38067=ORIENTED_EDGE ( 'NONE', *, *, #15652, .T. ) ;
#38097=VECTOR ( 'NONE', #40520, 1000.000000000000000 ) ;
#38112=CARTESIAN_POINT ( 'NONE',  ( 89.12784890491134604, -25.23119213852205789, -15.24166438581092109 ) ) ;
#38130=PLANE ( 'NONE',  #32060 ) ;
#38132=VERTEX_POINT ( 'NONE', #23996 ) ;
#38133=CIRCLE ( 'NONE', #38867, 2.000000000000000444 ) ;
#38150=VERTEX_POINT ( 'NONE', #34447 ) ;
#38172=DIRECTION ( 'NONE',  ( 0.000000000000000000, -0.3818493186865927203, 0.9242245927363029745 ) ) ;
#38190=EDGE_CURVE ( 'NONE', #2587, #2194, #30823, .T. ) ;
#38207=CARTESIAN_POINT ( 'NONE',  ( 85.82015659721905365, -27.84333996136784961, -14.15691383771150136 ) ) ;
#38255=ORIENTED_EDGE ( 'NONE', *, *, #5533, .F. ) ;
#38274=CARTESIAN_POINT ( 'NONE',  ( 84.49707967414211396, -25.99489077589524300, -13.39321520033831625 ) ) ;
#38275=DIRECTION ( 'NONE',  ( 0.000000000000000000, -0.9242245927363028635, -0.3818493186865930533 ) ) ;
#38277=DIRECTION ( 'NONE',  ( 1.000000000000000000, 0.000000000000000000, -0.000000000000000000 ) ) ;
#38359=ORIENTED_EDGE ( 'NONE', *, *, #31987, .T. ) ;
#38363=VERTEX_POINT ( 'NONE', #7768 ) ;
#38373=AXIS2_PLACEMENT_3D ( 'NONE', #8607, #28464, #39621 ) ;
#38381=CARTESIAN_POINT ( 'NONE',  ( 86.48169505875749508, -25.99489077589524300, -13.39321520033831625 ) ) ;
#38382=FACE_OUTER_BOUND ( 'NONE', #6155, .T. ) ;
#38390=VECTOR ( 'NONE', #5572, 1000.000000000000114 ) ;
#38421=EDGE_CURVE ( 'NONE', #29406, #13199, #28298, .T. ) ;
#38422=EDGE_CURVE ( 'NONE', #25709, #17452, #40494, .T. ) ;
#38423=EDGE_CURVE ( 'NONE', #5495, #22604, #4798, .T. ) ;
#38426=DIRECTION ( 'NONE',  ( 1.000000000000000000, 0.000000000000000000, -0.000000000000000000 ) ) ;
#38431=CARTESIAN_POINT ( 'NONE',  ( 91.77400275106518279, -25.99489077589524300, -13.39321520033831625 ) ) ;
#38467=DIRECTION ( 'NONE',  ( 0.000000000000000000, -0.9242245927363029745, -0.3818493186865927758 ) ) ;
#38470=CARTESIAN_POINT ( 'NONE',  ( 91.38554522942851577, -25.99489077589524300, -13.39321520033831625 ) ) ;
#38481=DIRECTION ( 'NONE',  ( 0.000000000000000000, -0.3818493186865927203, 0.9242245927363029745 ) ) ;
#38487=DIRECTION ( 'NONE',  ( 1.000000000000000000, 0.000000000000000000, -0.000000000000000000 ) ) ;
#38516=FACE_OUTER_BOUND ( 'NONE', #21768, .T. ) ;
#38527=ADVANCED_FACE ( 'NONE', ( #18488 ), #43381, .T. ) ;
#38528=AXIS2_PLACEMENT_3D ( 'NONE', #41906, #21146, #35251 ) ;
#38530=VECTOR ( 'NONE', #37953, 1000.000000000000114 ) ;
#38573=DIRECTION ( 'NONE',  ( 1.000000000000000000, 0.000000000000000000, -0.000000000000000000 ) ) ;
#38599=DIRECTION ( 'NONE',  ( 0.000000000000000000, -0.3818493186865927203, 0.9242245927363029745 ) ) ;
#38620=LINE ( 'NONE', #21765, #40091 ) ;
#38627=AXIS2_PLACEMENT_3D ( 'NONE', #37568, #34139, #5426 ) ;
#38632=AXIS2_PLACEMENT_3D ( 'NONE', #3529, #20869, #18343 ) ;
#38642=LINE ( 'NONE', #41659, #4015 ) ;
#38651=AXIS2_PLACEMENT_3D ( 'NONE', #10486, #24388, #14566 ) ;
#38668=CONICAL_SURFACE ( 'NONE', #16836, 1.610000000000000986, 0.9599310885968765916 ) ;
#38672=CARTESIAN_POINT ( 'NONE',  ( 87.14323352029596492, -25.99489077589524300, -13.39321520033831625 ) ) ;
#38684=FACE_OUTER_BOUND ( 'NONE', #40835, .T. ) ;
#38694=CARTESIAN_POINT ( 'NONE',  ( 85.15861813568058380, -25.99489077589524300, -13.39321520033831625 ) ) ;
#38707=DIRECTION ( 'NONE',  ( 0.000000000000000000, -0.3818493186865936084, 0.9242245927363024194 ) ) ;
#38730=DIRECTION ( 'NONE',  ( 0.5735764363510498232, -0.3127926500124802445, 0.7570804645221007600 ) ) ;
#38757=ORIENTED_EDGE ( 'NONE', *, *, #14764, .T. ) ;
#38776=DIRECTION ( 'NONE',  ( 0.000000000000000000, -0.9242245927363029745, -0.3818493186865927203 ) ) ;
#38783=VERTEX_POINT ( 'NONE', #20066 ) ;
#38786=CARTESIAN_POINT ( 'NONE',  ( 94.20708369096698220, -27.10035099198479358, -13.29271931396930739 ) ) ;
#38787=DIRECTION ( 'NONE',  ( 0.5735764363510499342, 0.3127926500124801890, -0.7570804645221008711 ) ) ;
#38793=ORIENTED_EDGE ( 'NONE', *, *, #4136, .T. ) ;
#38798=EDGE_CURVE ( 'NONE', #15657, #25112, #16876, .T. ) ;
#38810=ORIENTED_EDGE ( 'NONE', *, *, #7243, .T. ) ;
#38823=CARTESIAN_POINT ( 'NONE',  ( 84.38170309240724976, -25.23119213852205789, -15.24166438581092109 ) ) ;
#38825=CIRCLE ( 'NONE', #23559, 4.000000000000000888 ) ;
#38833=AXIS2_PLACEMENT_3D ( 'NONE', #39388, #14539, #17960 ) ;
#38835=CARTESIAN_POINT ( 'NONE',  ( 92.32016463086877422, -27.84333996136784961, -14.15691383771150136 ) ) ;
#38844=CARTESIAN_POINT ( 'NONE',  ( 121.9470836909669913, -25.99489077589524300, -13.39321520033831447 ) ) ;
#38847=EDGE_LOOP ( 'NONE', ( #36811, #986, #25830, #7400 ) ) ;
#38851=ADVANCED_FACE ( 'NONE', ( #2719 ), #16645, .F. ) ;
#38867=AXIS2_PLACEMENT_3D ( 'NONE', #1745, #5614, #22501 ) ;
#38937=EDGE_CURVE ( 'NONE', #44761, #10907, #41985, .T. ) ;
#38969=CARTESIAN_POINT ( 'NONE',  ( 86.48169505875749508, -25.99489077589524300, -13.39321520033831625 ) ) ;
#38991=ADVANCED_FACE ( 'NONE', ( #7709 ), #39792, .T. ) ;
#39022=AXIS2_PLACEMENT_3D ( 'NONE', #27518, #34553, #17255 ) ;
#39026=ORIENTED_EDGE ( 'NONE', *, *, #15579, .F. ) ;
#39042=EDGE_CURVE ( 'NONE', #21831, #35857, #4074, .T. ) ;
#39046=AXIS2_PLACEMENT_3D ( 'NONE', #42379, #21621, #11143 ) ;
#39054=VERTEX_POINT ( 'NONE', #12043 ) ;
#39069=AXIS2_PLACEMENT_3D ( 'NONE', #717, #28556, #42461 ) ;
#39080=CIRCLE ( 'NONE', #31810, 2.000000000000000444 ) ;
#39082=LINE ( 'NONE', #35189, #9929 ) ;
#39088=CARTESIAN_POINT ( 'NONE',  ( 121.9470836909669913, -25.99489077589524300, -13.39321520033831447 ) ) ;
#39093=ORIENTED_EDGE ( 'NONE', *, *, #33687, .T. ) ;
#39095=DIRECTION ( 'NONE',  ( 0.000000000000000000, -0.3818493186865927203, 0.9242245927363029745 ) ) ;
#39145=ORIENTED_EDGE ( 'NONE', *, *, #27338, .F. ) ;
#39176=DIRECTION ( 'NONE',  ( 0.000000000000000000, -0.9242245927363029745, -0.3818493186865929978 ) ) ;
#39186=FACE_OUTER_BOUND ( 'NONE', #26599, .T. ) ;
#39199=SURFACE_SIDE_STYLE ('',( #4988 ) ) ;
#39203=DIRECTION ( 'NONE',  ( 1.000000000000000000, 0.000000000000000000, -0.000000000000000000 ) ) ;
#39210=VERTEX_POINT ( 'NONE', #20237 ) ;
#39217=VERTEX_POINT ( 'NONE', #45076 ) ;
#39224=CARTESIAN_POINT ( 'NONE',  ( 86.48169505875749508, -27.84333996136784961, -14.15691383771150136 ) ) ;
#39245=CARTESIAN_POINT ( 'NONE',  ( 86.48169505875749508, -26.75858941326842810, -11.54476601486570964 ) ) ;
#39281=ORIENTED_EDGE ( 'NONE', *, *, #12244, .T. ) ;
#39288=DIRECTION ( 'NONE',  ( 0.000000000000000000, -0.3818493186865927203, 0.9242245927363029745 ) ) ;
#39295=VECTOR ( 'NONE', #4581, 1000.000000000000227 ) ;
#39306=FACE_OUTER_BOUND ( 'NONE', #36784, .T. ) ;
#39315=AXIS2_PLACEMENT_3D ( 'NONE', #5170, #19542, #9286 ) ;
#39328=EDGE_CURVE ( 'NONE', #10907, #44761, #40524, .T. ) ;
#39331=CIRCLE ( 'NONE', #30611, 0.8509999999999994236 ) ;
#39335=DIRECTION ( 'NONE',  ( 0.000000000000000000, -0.3818493186865927203, 0.9242245927363029745 ) ) ;
#39353=ORIENTED_EDGE ( 'NONE', *, *, #28729, .T. ) ;
#39354=CARTESIAN_POINT ( 'NONE',  ( 84.77016061404391678, -25.38011337280982715, -14.88121679464376257 ) ) ;
#39366=AXIS2_PLACEMENT_3D ( 'NONE', #38672, #6562, #27993 ) ;
#39388=CARTESIAN_POINT ( 'NONE',  ( 94.99177781699742695, -25.99489077589524300, -13.39321520033831447 ) ) ;
#39425=ORIENTED_EDGE ( 'NONE', *, *, #19177, .F. ) ;
#39433=SURFACE_STYLE_USAGE ( .BOTH. , #39199 ) ;
#39451=DIRECTION ( 'NONE',  ( 1.000000000000000000, 0.000000000000000000, -0.000000000000000000 ) ) ;
#39466=DIRECTION ( 'NONE',  ( 0.5735764363510499342, 0.3127926500124801890, -0.7570804645221008711 ) ) ;
#39475=DIRECTION ( 'NONE',  ( 1.000000000000000000, 0.000000000000000000, -0.000000000000000000 ) ) ;
#39489=VERTEX_POINT ( 'NONE', #3564 ) ;
#39490=AXIS2_PLACEMENT_3D ( 'NONE', #25353, #35813, #35358 ) ;
#39499=EDGE_CURVE ( 'NONE', #19198, #13545, #4229, .T. ) ;
#39504=ORIENTED_EDGE ( 'NONE', *, *, #19090, .T. ) ;
#39509=ORIENTED_EDGE ( 'NONE', *, *, #16701, .F. ) ;
#39510=DIRECTION ( 'NONE',  ( -0.5735764363510450492, -0.3127926500124816878, 0.7570804645221038687 ) ) ;
#39514=EDGE_CURVE ( 'NONE', #28262, #38150, #14279, .T. ) ;
#39517=DIRECTION ( 'NONE',  ( 1.000000000000000000, 0.000000000000000000, -0.000000000000000000 ) ) ;
#39529=ORIENTED_EDGE ( 'NONE', *, *, #31987, .F. ) ;
#39561=FACE_OUTER_BOUND ( 'NONE', #10062, .T. ) ;
#39565=DIRECTION ( 'NONE',  ( 1.000000000000000000, 0.000000000000000000, -0.000000000000000000 ) ) ;
#39569=EDGE_CURVE ( 'NONE', #25709, #22099, #28415, .T. ) ;
#39585=AXIS2_PLACEMENT_3D ( 'NONE', #15203, #22266, #4929 ) ;
#39613=DIRECTION ( 'NONE',  ( 1.000000000000000000, 0.000000000000000000, -0.000000000000000000 ) ) ;
#39616=CLOSED_SHELL ( 'NONE', ( #11418, #30216, #29753, #28395, #13390, #33361, #40606, #18054, #8746, #18364, #31034, #7238, #22403, #38991, #21688, #21684, #6823, #30973, #12223, #21703, #10111, #33658, #25048, #21193, #44721, #11021, #19161, #30341, #34204, #42399, #35643, #30327, #17052, #11983, #21259, #12816, #38527, #44438, #51, #9706, #1850, #41229, #42144, #33943, #32307, #43980, #38851, #7755, #43490, #3993, #12417, #6699, #18336, #2446, #14196, #33928, #42850, #2864, #43247, #40962, #33055, #17608, #27948, #36214, #25355, #23981, #26110, #8049, #27114, #239, #8073, #22076, #10851, #15114, #32803, #22519, #31424, #5757, #13805, #2765, #4659, #2731, #10356, #10548, #5204, #21772, #43289, #12933, #1179, #12213, #28452, #8201, #9151, #13127, #1863, #31590, #33686, #10298, #4274, #6358, #8605, #34230, #39807, #18922, #22247, #2930, #13613, #13168, #29846, #35264, #13448, #16993, #6930, #19731 ) ) ;
#39619=ORIENTED_EDGE ( 'NONE', *, *, #28009, .F. ) ;
#39621=DIRECTION ( 'NONE',  ( 0.000000000000000000, -0.3818493186865927203, 0.9242245927363029745 ) ) ;
#39638=ORIENTED_EDGE ( 'NONE', *, *, #22472, .T. ) ;
#39672=EDGE_LOOP ( 'NONE', ( #3219, #6527, #31032, #17547, #18512 ) ) ;
#39678=AXIS2_PLACEMENT_3D ( 'NONE', #42827, #15226, #35508 ) ;
#39681=EDGE_CURVE ( 'NONE', #10759, #42482, #18044, .T. ) ;
#39694=DIRECTION ( 'NONE',  ( 1.000000000000000000, 0.000000000000000000, -0.000000000000000000 ) ) ;
#39697=ORIENTED_EDGE ( 'NONE', *, *, #23358, .F. ) ;
#39706=AXIS2_PLACEMENT_3D ( 'NONE', #1580, #43322, #25996 ) ;
#39729=CARTESIAN_POINT ( 'NONE',  ( 83.44708369096697709, -26.60966817898065884, -11.90521360603286816 ) ) ;
#39738=AXIS2_PLACEMENT_3D ( 'NONE', #13105, #37938, #20623 ) ;
#39744=VECTOR ( 'NONE', #28731, 1000.000000000000000 ) ;
#39755=LINE ( 'NONE', #9421, #36845 ) ;
#39770=VERTEX_POINT ( 'NONE', #21568 ) ;
#39778=DIRECTION ( 'NONE',  ( 1.000000000000000000, 0.000000000000000000, -0.000000000000000000 ) ) ;
#39781=CIRCLE ( 'NONE', #12862, 2.000000000000000444 ) ;
#39792=CONICAL_SURFACE ( 'NONE', #21567, 2.000000000000000444, 0.9599310885968830309 ) ;
#39805=AXIS2_PLACEMENT_3D ( 'NONE', #5004, #2031, #15957 ) ;
#39807=ADVANCED_FACE ( 'NONE', ( #35911 ), #28241, .T. ) ;
#39821=DIRECTION ( 'NONE',  ( 0.000000000000000000, -0.3818493186865927203, 0.9242245927363029745 ) ) ;
#39838=LINE ( 'NONE', #19314, #38097 ) ;
#39841=CARTESIAN_POINT ( 'NONE',  ( 94.20708369096698220, -25.17209684859101415, -13.61049647700816401 ) ) ;
#39875=EDGE_CURVE ( 'NONE', #31353, #32925, #4902, .T. ) ;
#39896=ORIENTED_EDGE ( 'NONE', *, *, #13019, .T. ) ;
#39903=DIRECTION ( 'NONE',  ( 1.000000000000000000, 0.000000000000000000, -0.000000000000000000 ) ) ;
#39948=ORIENTED_EDGE ( 'NONE', *, *, #22817, .T. ) ;
#39963=VERTEX_POINT ( 'NONE', #16542 ) ;
#39972=DIRECTION ( 'NONE',  ( 0.5735764363510498232, -0.3127926500124802445, 0.7570804645221007600 ) ) ;
#39985=DIRECTION ( 'NONE',  ( 1.000000000000000000, 0.000000000000000000, -0.000000000000000000 ) ) ;
#39989=ORIENTED_EDGE ( 'NONE', *, *, #5533, .T. ) ;
#40008=LINE ( 'NONE', #25660, #31685 ) ;
#40011=CARTESIAN_POINT ( 'NONE',  ( 84.38170309240724976, -26.75858941326842810, -11.54476601486570964 ) ) ;
#40072=CIRCLE ( 'NONE', #42264, 2.000000000000000444 ) ;
#40084=EDGE_CURVE ( 'NONE', #10139, #25112, #14400, .T. ) ;
#40089=CARTESIAN_POINT ( 'NONE',  ( 89.12784890491134604, -25.99489077589524300, -13.39321520033831625 ) ) ;
#40091=VECTOR ( 'NONE', #17673, 1000.000000000000000 ) ;
#40095=CIRCLE ( 'NONE', #15323, 2.000000000000000444 ) ;
#40110=CIRCLE ( 'NONE', #15380, 2.000000000000000444 ) ;
#40129=DIRECTION ( 'NONE',  ( -1.224775218828352108E-16, 0.9242245927363028635, 0.3818493186865928313 ) ) ;
#40139=VERTEX_POINT ( 'NONE', #29703 ) ;
#40156=CARTESIAN_POINT ( 'NONE',  ( 94.20708369096698220, -25.14343533174585943, -14.10537061818067883 ) ) ;
#40158=DIRECTION ( 'NONE',  ( 0.000000000000000000, -0.3818493186865927203, 0.9242245927363029745 ) ) ;
#40159=AXIS2_PLACEMENT_3D ( 'NONE', #271, #3473, #24446 ) ;
#40166=EDGE_LOOP ( 'NONE', ( #34966, #44206, #36163, #1382, #24011 ) ) ;
#40198=EDGE_CURVE ( 'NONE', #12976, #40373, #23870, .T. ) ;
#40223=CONICAL_SURFACE ( 'NONE', #33651, 2.000000000000000444, 0.9599310885968830309 ) ;
#40234=CARTESIAN_POINT ( 'NONE',  ( 87.41631446019775353, -25.99489077589524300, -13.39321520033831625 ) ) ;
#40245=EDGE_LOOP ( 'NONE', ( #42705, #8199, #16840, #24088, #13776, #15446 ) ) ;
#40248=CONICAL_SURFACE ( 'NONE', #20611, 1.610000000000000986, 0.9599310885968765916 ) ;
#40251=CARTESIAN_POINT ( 'NONE',  ( 89.78938736644981589, -26.75858941326842810, -11.54476601486570964 ) ) ;
#40264=DIRECTION ( 'NONE',  ( 0.000000000000000000, 0.3818493186865927203, -0.9242245927363029745 ) ) ;
#40265=DIRECTION ( 'NONE',  ( -0.000000000000000000, -0.9242245927363028635, -0.3818493186865929423 ) ) ;
#40267=CARTESIAN_POINT ( 'NONE',  ( 88.73939138327467901, -25.99489077589524300, -13.39321520033831625 ) ) ;
#40276=VECTOR ( 'NONE', #27378, 1000.000000000000114 ) ;
#40302=CONICAL_SURFACE ( 'NONE', #43928, 2.000000000000000444, 0.9599310885968830309 ) ;
#40316=CARTESIAN_POINT ( 'NONE',  ( 84.49707967414211396, -25.99489077589524300, -13.39321520033831625 ) ) ;
#40320=CARTESIAN_POINT ( 'NONE',  ( 89.78938736644981589, -25.99489077589524300, -13.39321520033831625 ) ) ;
#40336=AXIS2_PLACEMENT_3D ( 'NONE', #44063, #40870, #23304 ) ;
#40339=CYLINDRICAL_SURFACE ( 'NONE', #21381, 1.999999999999998890 ) ;
#40341=EDGE_CURVE ( 'NONE', #2587, #24723, #21659, .T. ) ;
#40373=VERTEX_POINT ( 'NONE', #5345 ) ;
#40404=CIRCLE ( 'NONE', #42581, 2.000000000000000444 ) ;
#40440=ORIENTED_EDGE ( 'NONE', *, *, #41214, .F. ) ;
#40442=DIRECTION ( 'NONE',  ( 0.000000000000000000, -0.3818493186865936084, 0.9242245927363024194 ) ) ;
#40447=CARTESIAN_POINT ( 'NONE',  ( 84.49707967414211396, -25.99489077589524300, -13.39321520033831625 ) ) ;
#40494=CIRCLE ( 'NONE', #9174, 6.426280380454326924 ) ;
#40498=FACE_OUTER_BOUND ( 'NONE', #23206, .T. ) ;
#40519=CIRCLE ( 'NONE', #29570, 2.000000000000000444 ) ;
#40520=DIRECTION ( 'NONE',  ( 1.000000000000000000, 0.000000000000000000, -0.000000000000000000 ) ) ;
#40522=CARTESIAN_POINT ( 'NONE',  ( 85.70478001548416103, -25.99489077589524300, -13.39321520033831447 ) ) ;
#40524=CIRCLE ( 'NONE', #7026, 4.000000000000000888 ) ;
#40527=CARTESIAN_POINT ( 'NONE',  ( 94.86797725101185108, -25.51174947080612654, -12.63637840582423166 ) ) ;
#40533=EDGE_CURVE ( 'NONE', #18672, #25132, #40923, .T. ) ;
#40537=ORIENTED_EDGE ( 'NONE', *, *, #20396, .T. ) ;
#40560=CONICAL_SURFACE ( 'NONE', #15060, 2.000000000000000444, 0.9599310885968830309 ) ;
#40570=DIRECTION ( 'NONE',  ( 0.000000000000000000, -0.9242245927363028635, -0.3818493186865930533 ) ) ;
#40574=CARTESIAN_POINT ( 'NONE',  ( 84.38170309240724976, -25.99489077589524300, -13.39321520033831447 ) ) ;
#40585=DIRECTION ( 'NONE',  ( 1.000000000000000000, 1.131967377815149893E-16, 4.676795828538290169E-17 ) ) ;
#40606=ADVANCED_FACE ( 'NONE', ( #27461 ), #31869, .T. ) ;
#40615=AXIS2_PLACEMENT_3D ( 'NONE', #8783, #16079, #29308 ) ;
#40661=EDGE_CURVE ( 'NONE', #33578, #13545, #23167, .T. ) ;
#40666=CARTESIAN_POINT ( 'NONE',  ( 87.14323352029596492, -25.99489077589524300, -13.39321520033831625 ) ) ;
#40709=ORIENTED_EDGE ( 'NONE', *, *, #13949, .F. ) ;
#40727=DIRECTION ( 'NONE',  ( -0.5735764363510446051, 0.3127926500124816878, -0.7570804645221042017 ) ) ;
#40745=FACE_OUTER_BOUND ( 'NONE', #6501, .T. ) ;
#40775=VECTOR ( 'NONE', #10992, 1000.000000000000114 ) ;
#40784=ORIENTED_EDGE ( 'NONE', *, *, #22523, .T. ) ;
#40786=DIRECTION ( 'NONE',  ( 0.000000000000000000, -0.3818493186865927203, 0.9242245927363029745 ) ) ;
#40787=ORIENTED_EDGE ( 'NONE', *, *, #6638, .T. ) ;
#40806=ORIENTED_EDGE ( 'NONE', *, *, #13435, .T. ) ;
#40808=CIRCLE ( 'NONE', #5078, 2.000000000000000444 ) ;
#40810=DIRECTION ( 'NONE',  ( 0.000000000000000000, -0.3818493186865927203, 0.9242245927363029745 ) ) ;
#40835=EDGE_LOOP ( 'NONE', ( #20674, #10890, #29371, #3500, #19181 ) ) ;
#40844=DIRECTION ( 'NONE',  ( -1.224775218828351615E-16, 0.3818493186865896116, -0.9242245927363041957 ) ) ;
#40847=AXIS2_PLACEMENT_3D ( 'NONE', #6336, #43743, #20253 ) ;
#40853=ORIENTED_EDGE ( 'NONE', *, *, #15006, .T. ) ;
#40855=VECTOR ( 'NONE', #40727, 1000.000000000000114 ) ;
#40866=ORIENTED_EDGE ( 'NONE', *, *, #3466, .T. ) ;
#40870=DIRECTION ( 'NONE',  ( 1.000000000000000000, 0.000000000000000000, -0.000000000000000000 ) ) ;
#40879=ORIENTED_EDGE ( 'NONE', *, *, #29, .T. ) ;
#40892=CARTESIAN_POINT ( 'NONE',  ( 96.21525317080913453, -23.96406343964327590, -13.11138972548619641 ) ) ;
#40899=EDGE_CURVE ( 'NONE', #12518, #31222, #42784, .T. ) ;
#40907=( NAMED_UNIT ( * ) PLANE_ANGLE_UNIT ( ) SI_UNIT ( $, .RADIAN. ) );
#40923=LINE ( 'NONE', #17635, #16594 ) ;
#40927=ORIENTED_EDGE ( 'NONE', *, *, #7754, .F. ) ;
#40943=ORIENTED_EDGE ( 'NONE', *, *, #8438, .T. ) ;
#40945=DIRECTION ( 'NONE',  ( 0.000000000000000000, -0.9242245927363028635, -0.3818493186865930533 ) ) ;
#40949=DIRECTION ( 'NONE',  ( -0.5735764363510446051, 0.3127926500124816878, -0.7570804645221042017 ) ) ;
#40962=ADVANCED_FACE ( 'NONE', ( #26573 ), #9470, .T. ) ;
#40979=DIRECTION ( 'NONE',  ( 1.000000000000000000, 0.000000000000000000, -0.000000000000000000 ) ) ;
#40987=AXIS2_PLACEMENT_3D ( 'NONE', #28519, #18018, #11188 ) ;
#41003=CARTESIAN_POINT ( 'NONE',  ( 83.44708369096697709, -25.99489077589524300, -13.39321520033831625 ) ) ;
#41024=ORIENTED_EDGE ( 'NONE', *, *, #43948, .T. ) ;
#41025=AXIS2_PLACEMENT_3D ( 'NONE', #8325, #42091, #22002 ) ;
#41035=DIRECTION ( 'NONE',  ( 1.000000000000000000, 0.000000000000000000, -0.000000000000000000 ) ) ;
#41036=VERTEX_POINT ( 'NONE', #33162 ) ;
#41041=ORIENTED_EDGE ( 'NONE', *, *, #3091, .F. ) ;
#41045=DIRECTION ( 'NONE',  ( 1.000000000000000000, 0.000000000000000000, -0.000000000000000000 ) ) ;
#41064=DIRECTION ( 'NONE',  ( -1.000000000000000000, 0.000000000000000000, 0.000000000000000000 ) ) ;
#41072=AXIS2_PLACEMENT_3D ( 'NONE', #5668, #30524, #9330 ) ;
#41120=ORIENTED_EDGE ( 'NONE', *, *, #41198, .F. ) ;
#41131=EDGE_LOOP ( 'NONE', ( #6476, #9387, #42928, #13792, #17351 ) ) ;
#41140=ORIENTED_EDGE ( 'NONE', *, *, #19090, .F. ) ;
#41141=AXIS2_PLACEMENT_3D ( 'NONE', #4511, #42155, #32544 ) ;
#41157=DIRECTION ( 'NONE',  ( 0.000000000000000000, -0.9242245927363029745, -0.3818493186865927758 ) ) ;
#41162=VERTEX_POINT ( 'NONE', #29539 ) ;
#41168=CARTESIAN_POINT ( 'NONE',  ( 92.32016463086877422, -25.99489077589524300, -13.39321520033831447 ) ) ;
#41193=VECTOR ( 'NONE', #14272, 1000.000000000000000 ) ;
#41198=EDGE_CURVE ( 'NONE', #10961, #42332, #20115, .T. ) ;
#41214=EDGE_CURVE ( 'NONE', #7248, #2572, #21534, .T. ) ;
#41227=DIRECTION ( 'NONE',  ( 1.000000000000000000, 0.000000000000000000, -0.000000000000000000 ) ) ;
#41229=ADVANCED_FACE ( 'NONE', ( #8795 ), #8447, .F. ) ;
#41265=AXIS2_PLACEMENT_3D ( 'NONE', #18687, #33189, #15730 ) ;
#41302=ORIENTED_EDGE ( 'NONE', *, *, #41794, .F. ) ;
#41310=EDGE_CURVE ( 'NONE', #35058, #19992, #36598, .T. ) ;
#41324=AXIS2_PLACEMENT_3D ( 'NONE', #36632, #5623, #26613 ) ;
#41334=DIRECTION ( 'NONE',  ( 0.5735764363510498232, -0.3127926500124802445, 0.7570804645221007600 ) ) ;
#41344=DIRECTION ( 'NONE',  ( -0.5735764363510446051, 0.3127926500124816878, -0.7570804645221042017 ) ) ;
#41351=VERTEX_POINT ( 'NONE', #9477 ) ;
#41398=CARTESIAN_POINT ( 'NONE',  ( 121.9470836909669913, -25.99489077589524300, -13.39321520033831447 ) ) ;
#41436=LINE ( 'NONE', #17039, #5616 ) ;
#41444=CARTESIAN_POINT ( 'NONE',  ( 96.46827370896536991, -26.80223900086530264, -12.78781649172082879 ) ) ;
#41454=DIRECTION ( 'NONE',  ( 0.000000000000000000, 0.9242245927363028635, 0.3818493186865930533 ) ) ;
#41465=ORIENTED_EDGE ( 'NONE', *, *, #27287, .F. ) ;
#41468=ORIENTED_EDGE ( 'NONE', *, *, #27538, .T. ) ;
#41474=AXIS2_PLACEMENT_3D ( 'NONE', #18554, #1880, #32885 ) ;
#41488=DIRECTION ( 'NONE',  ( 0.000000000000000000, 0.3818493186865927203, -0.9242245927363029745 ) ) ;
#41503=B_SPLINE_CURVE_WITH_KNOTS ( 'NONE', 3,
 ( #23610, #36587, #15860, #5362 ),
 .UNSPECIFIED., .F., .F.,
 ( 4, 4 ),
 ( 0.000000000000000000, 1.000000000000000000 ),
 .UNSPECIFIED. ) ;
#41525=DIRECTION ( 'NONE',  ( 0.000000000000000000, -0.3818493186865927203, 0.9242245927363029745 ) ) ;
#41527=DIRECTION ( 'NONE',  ( 0.000000000000000000, 0.3818493186865928868, -0.9242245927363027524 ) ) ;
#41531=AXIS2_PLACEMENT_3D ( 'NONE', #15700, #11831, #14798 ) ;
#41541=ORIENTED_EDGE ( 'NONE', *, *, #10088, .T. ) ;
#41617=DIRECTION ( 'NONE',  ( 0.000000000000000000, -0.3818493186865936084, 0.9242245927363024194 ) ) ;
#41630=AXIS2_PLACEMENT_3D ( 'NONE', #43211, #33368, #25880 ) ;
#41633=DIRECTION ( 'NONE',  ( 1.000000000000000000, 0.000000000000000000, -0.000000000000000000 ) ) ;
#41647=ORIENTED_EDGE ( 'NONE', *, *, #28963, .F. ) ;
#41652=ORIENTED_EDGE ( 'NONE', *, *, #25481, .T. ) ;
#41659=CARTESIAN_POINT ( 'NONE',  ( 89.78938736644981589, -25.23119213852205789, -15.24166438581092109 ) ) ;
#41666=VECTOR ( 'NONE', #422, 1000.000000000000000 ) ;
#41697=DIRECTION ( 'NONE',  ( 1.000000000000000000, 0.000000000000000000, -0.000000000000000000 ) ) ;
#41727=VERTEX_POINT ( 'NONE', #4641 ) ;
#41736=DIRECTION ( 'NONE',  ( 0.000000000000000000, 0.9242245927363041957, 0.3818493186865896116 ) ) ;
#41778=EDGE_CURVE ( 'NONE', #26284, #25225, #39082, .T. ) ;
#41794=EDGE_CURVE ( 'NONE', #3780, #14434, #31785, .T. ) ;
#41797=ORIENTED_EDGE ( 'NONE', *, *, #40661, .T. ) ;
#41799=CARTESIAN_POINT ( 'NONE',  ( 83.83554121260367253, -25.99489077589524300, -13.39321520033831625 ) ) ;
#41804=EDGE_CURVE ( 'NONE', #4353, #22394, #40519, .T. ) ;
#41808=ORIENTED_EDGE ( 'NONE', *, *, #36446, .F. ) ;
#41810=EDGE_CURVE ( 'NONE', #42505, #20212, #39755, .T. ) ;
#41814=EDGE_LOOP ( 'NONE', ( #22383, #17412, #43611, #35532, #40853 ) ) ;
#41815=DIRECTION ( 'NONE',  ( -1.000000000000000000, 0.000000000000000000, 0.000000000000000000 ) ) ;
#41842=EDGE_CURVE ( 'NONE', #17452, #2933, #31746, .T. ) ;
#41858=EDGE_LOOP ( 'NONE', ( #14826, #20837, #25815, #1486, #22306, #33758 ) ) ;
#41864=EDGE_CURVE ( 'NONE', #36515, #38150, #8481, .T. ) ;
#41871=DIRECTION ( 'NONE',  ( -0.8949343913984424415, 0.4123869368673875324, 0.1703803081152070742 ) ) ;
#41872=DIRECTION ( 'NONE',  ( 0.000000000000000000, -0.3818493186865927203, 0.9242245927363029745 ) ) ;
#41881=CARTESIAN_POINT ( 'NONE',  ( 121.9470836909669913, -24.14644159042263993, -12.62951656296512937 ) ) ;
#41888=CARTESIAN_POINT ( 'NONE',  ( 91.77400275106518279, -27.84333996136784961, -14.15691383771150136 ) ) ;
#41906=CARTESIAN_POINT ( 'NONE',  ( 94.20708369096698220, -25.99489077589524300, -13.39321520033831447 ) ) ;
#41907=CONICAL_SURFACE ( 'NONE', #44090, 1.610000000000000986, 0.9599310885968765916 ) ;
#41931=AXIS2_PLACEMENT_3D ( 'NONE', #31809, #17689, #35673 ) ;
#41955=LINE ( 'NONE', #16899, #20622 ) ;
#41961=DIRECTION ( 'NONE',  ( 0.000000000000000000, -0.3818493186865936084, 0.9242245927363024194 ) ) ;
#41968=CIRCLE ( 'NONE', #41265, 6.479565957685751165 ) ;
#41969=CARTESIAN_POINT ( 'NONE',  ( 94.20708369096698220, -24.88943055980569241, -13.49371108670732333 ) ) ;
#41985=CIRCLE ( 'NONE', #39046, 4.000000000000000888 ) ;
#41987=CARTESIAN_POINT ( 'NONE',  ( 87.80477198183443477, -26.75858941326842810, -11.54476601486570964 ) ) ;
#42013=FACE_OUTER_BOUND ( 'NONE', #11917, .T. ) ;
#42024=AXIS2_PLACEMENT_3D ( 'NONE', #44709, #18396, #42564 ) ;
#42029=CARTESIAN_POINT ( 'NONE',  ( 96.54708369096698561, -24.20446030063578391, -12.09626349990295147 ) ) ;
#42041=CARTESIAN_POINT ( 'NONE',  ( 86.48169505875749508, -25.99489077589524300, -13.39321520033831625 ) ) ;
#42044=CIRCLE ( 'NONE', #11456, 2.000000000000000444 ) ;
#42058=ORIENTED_EDGE ( 'NONE', *, *, #33820, .T. ) ;
#42082=DIRECTION ( 'NONE',  ( 0.000000000000000000, 0.3818493186865927203, -0.9242245927363029745 ) ) ;
#42091=DIRECTION ( 'NONE',  ( 1.000000000000000000, 0.000000000000000000, -0.000000000000000000 ) ) ;
#42108=CARTESIAN_POINT ( 'NONE',  ( 90.99708770779186295, -25.99489077589524300, -13.39321520033831447 ) ) ;
#42112=EDGE_CURVE ( 'NONE', #36351, #10961, #39781, .T. ) ;
#42125=CARTESIAN_POINT ( 'NONE',  ( 85.70478001548416103, -25.99489077589524300, -13.39321520033831447 ) ) ;
#42141=DIRECTION ( 'NONE',  ( 1.000000000000000000, 0.000000000000000000, -0.000000000000000000 ) ) ;
#42144=ADVANCED_FACE ( 'NONE', ( #34905 ), #20154, .F. ) ;
#42155=DIRECTION ( 'NONE',  ( 1.000000000000000000, 0.000000000000000000, -0.000000000000000000 ) ) ;
#42159=DIRECTION ( 'NONE',  ( 1.000000000000000000, 0.000000000000000000, -0.000000000000000000 ) ) ;
#42161=CARTESIAN_POINT ( 'NONE',  ( 90.04708369096697140, -25.99489077589524300, -13.39321520033831447 ) ) ;
#42171=VERTEX_POINT ( 'NONE', #23576 ) ;
#42185=CARTESIAN_POINT ( 'NONE',  ( 0.000000000000000000, 0.000000000000000000, 0.000000000000000000 ) ) ;
#42191=VERTEX_POINT ( 'NONE', #2804 ) ;
#42209=EDGE_CURVE ( 'NONE', #29623, #21444, #44893, .T. ) ;
#42228=CARTESIAN_POINT ( 'NONE',  ( 121.9470836909669913, -24.14644159042263993, -12.62951656296512937 ) ) ;
#42241=DIRECTION ( 'NONE',  ( 0.000000000000000000, -0.9242245927363028635, -0.3818493186865930533 ) ) ;
#42246=AXIS2_PLACEMENT_3D ( 'NONE', #20924, #38020, #161 ) ;
#42247=LINE ( 'NONE', #13982, #28813 ) ;
#42260=ORIENTED_EDGE ( 'NONE', *, *, #782, .F. ) ;
#42264=AXIS2_PLACEMENT_3D ( 'NONE', #30512, #19803, #40786 ) ;
#42279=CARTESIAN_POINT ( 'NONE',  ( 88.46631044337289040, -25.99489077589524300, -13.39321520033831625 ) ) ;
#42312=CIRCLE ( 'NONE', #13193, 1.610000000000000986 ) ;
#42325=CONICAL_SURFACE ( 'NONE', #27751, 1.610000000000000986, 0.9599310885968765916 ) ;
#42326=DIRECTION ( 'NONE',  ( 0.000000000000000000, -0.9242245927363040847, -0.3818493186865897226 ) ) ;
#42332=VERTEX_POINT ( 'NONE', #13533 ) ;
#42355=DIRECTION ( 'NONE',  ( 0.000000000000000000, -0.3818493186865927203, 0.9242245927363029745 ) ) ;
#42370=ORIENTED_EDGE ( 'NONE', *, *, #40899, .T. ) ;
#42379=CARTESIAN_POINT ( 'NONE',  ( 94.99177781699742695, -25.99489077589524300, -13.39321520033831447 ) ) ;
#42386=ORIENTED_EDGE ( 'NONE', *, *, #21820, .T. ) ;
#42389=FACE_OUTER_BOUND ( 'NONE', #6002, .T. ) ;
#42394=ORIENTED_EDGE ( 'NONE', *, *, #33687, .F. ) ;
#42397=FACE_OUTER_BOUND ( 'NONE', #41814, .T. ) ;
#42399=ADVANCED_FACE ( 'NONE', ( #42013 ), #4814, .T. ) ;
#42422=CARTESIAN_POINT ( 'NONE',  ( 84.77016061404391678, -26.60966817898065884, -11.90521360603286816 ) ) ;
#42427=AXIS2_PLACEMENT_3D ( 'NONE', #31835, #604, #24774 ) ;
#42433=CARTESIAN_POINT ( 'NONE',  ( 87.80477198183443477, -25.99489077589524300, -13.39321520033831625 ) ) ;
#42434=CARTESIAN_POINT ( 'NONE',  ( 91.38554522942851577, -25.99489077589524300, -13.39321520033831625 ) ) ;
#42442=ORIENTED_EDGE ( 'NONE', *, *, #14261, .T. ) ;
#42461=DIRECTION ( 'NONE',  ( 0.000000000000000000, -0.3818493186865927203, 0.9242245927363029745 ) ) ;
#42467=UNCERTAINTY_MEASURE_WITH_UNIT (LENGTH_MEASURE( 1.000000000000000082E-05 ), #25819, 'distance_accuracy_value', 'NONE');
#42473=EDGE_CURVE ( 'NONE', #43753, #30603, #31035, .T. ) ;
#42474=CARTESIAN_POINT ( 'NONE',  ( 91.65862616933031859, -25.99489077589524300, -13.39321520033831447 ) ) ;
#42476=ORIENTED_EDGE ( 'NONE', *, *, #1121, .T. ) ;
#42482=VERTEX_POINT ( 'NONE', #42685 ) ;
#42501=AXIS2_PLACEMENT_3D ( 'NONE', #18420, #15442, #7460 ) ;
#42505=VERTEX_POINT ( 'NONE', #11000 ) ;
#42511=FACE_OUTER_BOUND ( 'NONE', #11544, .T. ) ;
#42512=CARTESIAN_POINT ( 'NONE',  ( 90.72400676789006013, -25.99489077589524300, -13.39321520033831625 ) ) ;
#42514=ORIENTED_EDGE ( 'NONE', *, *, #34728, .T. ) ;
#42532=ORIENTED_EDGE ( 'NONE', *, *, #36180, .T. ) ;
#42564=DIRECTION ( 'NONE',  ( 0.000000000000000000, -0.9242245927363028635, -0.3818493186865930533 ) ) ;
#42581=AXIS2_PLACEMENT_3D ( 'NONE', #22295, #32325, #11588 ) ;
#42587=EDGE_LOOP ( 'NONE', ( #20175, #27177, #36294, #27277, #10277, #33134 ) ) ;
#42588=EDGE_CURVE ( 'NONE', #30333, #37160, #36876, .T. ) ;
#42609=DIRECTION ( 'NONE',  ( -1.000000000000000000, 0.000000000000000000, 0.000000000000000000 ) ) ;
#42621=CARTESIAN_POINT ( 'NONE',  ( 87.14323352029596492, -25.99489077589524300, -13.39321520033831625 ) ) ;
#42634=DIRECTION ( 'NONE',  ( -0.8949343913984424415, -0.1703803081152067966, 0.4123869368673871993 ) ) ;
#42654=DIRECTION ( 'NONE',  ( 1.000000000000000000, 0.000000000000000000, -0.000000000000000000 ) ) ;
#42664=EDGE_CURVE ( 'NONE', #25132, #5495, #31772, .T. ) ;
#42665=ORIENTED_EDGE ( 'NONE', *, *, #5645, .F. ) ;
#42677=CARTESIAN_POINT ( 'NONE',  ( 88.73939138327467901, -25.38011337280982715, -14.88121679464376257 ) ) ;
#42685=CARTESIAN_POINT ( 'NONE',  ( 96.21525317080913453, -28.02571811214721009, -13.67504067519043431 ) ) ;
#42704=ORIENTED_EDGE ( 'NONE', *, *, #34603, .F. ) ;
#42705=ORIENTED_EDGE ( 'NONE', *, *, #18048, .T. ) ;
#42712=ORIENTED_EDGE ( 'NONE', *, *, #16411, .T. ) ;
#42725=DIRECTION ( 'NONE',  ( 0.000000000000000000, -0.9242245927363028635, -0.3818493186865930533 ) ) ;
#42738=VECTOR ( 'NONE', #33854, 1000.000000000000114 ) ;
#42784=LINE ( 'NONE', #39354, #5665 ) ;
#42815=VERTEX_POINT ( 'NONE', #26480 ) ;
#42821=AXIS2_PLACEMENT_3D ( 'NONE', #22694, #30219, #9022 ) ;
#42827=CARTESIAN_POINT ( 'NONE',  ( 88.35093386163799778, -25.99489077589524300, -13.39321520033831447 ) ) ;
#42847=DIRECTION ( 'NONE',  ( 1.000000000000000000, 0.000000000000000000, 0.000000000000000000 ) ) ;
#42850=ADVANCED_FACE ( 'NONE', ( #44942 ), #6625, .T. ) ;
#42861=EDGE_LOOP ( 'NONE', ( #40787, #3867, #38067, #3896, #24881, #3253, #44924, #21607, #9633, #27663, #30324, #31031, #39529 ) ) ;
#42890=LINE ( 'NONE', #21908, #24937 ) ;
#42907=VERTEX_POINT ( 'NONE', #2518 ) ;
#42913=PRODUCT_DEFINITION_CONTEXT ( 'detailed design', #33198, 'design' ) ;
#42928=ORIENTED_EDGE ( 'NONE', *, *, #28009, .T. ) ;
#42955=ORIENTED_EDGE ( 'NONE', *, *, #37861, .T. ) ;
#42966=EDGE_CURVE ( 'NONE', #41162, #9931, #19413, .T. ) ;
#42972=ORIENTED_EDGE ( 'NONE', *, *, #19438, .F. ) ;
#42973=DIRECTION ( 'NONE',  ( 1.000000000000000000, 0.000000000000000000, -0.000000000000000000 ) ) ;
#42991=DIRECTION ( 'NONE',  ( 1.000000000000000000, 0.000000000000000000, -0.000000000000000000 ) ) ;
#43008=AXIS2_PLACEMENT_3D ( 'NONE', #11450, #35815, #32177 ) ;
#43017=CARTESIAN_POINT ( 'NONE',  ( 86.09323753712084226, -25.38011337280982715, -14.88121679464376257 ) ) ;
#43021=CIRCLE ( 'NONE', #5156, 1.610000000000000986 ) ;
#43033=ORIENTED_EDGE ( 'NONE', *, *, #30872, .T. ) ;
#43036=ORIENTED_EDGE ( 'NONE', *, *, #39042, .F. ) ;
#43083=VECTOR ( 'NONE', #2565, 1000.000000000000000 ) ;
#43089=COLOUR_RGB ( '',0.7921568627450980005, 0.8196078431372548767, 0.9333333333333333481 ) ;
#43094=FACE_OUTER_BOUND ( 'NONE', #22135, .T. ) ;
#43100=VECTOR ( 'NONE', #17790, 999.9999999999998863 ) ;
#43119=LINE ( 'NONE', #28770, #39295 ) ;
#43151=DIRECTION ( 'NONE',  ( 0.000000000000000000, 0.3818493186865928868, -0.9242245927363027524 ) ) ;
#43154=LINE ( 'NONE', #8498, #25944 ) ;
#43164=ORIENTED_EDGE ( 'NONE', *, *, #11932, .F. ) ;
#43196=EDGE_LOOP ( 'NONE', ( #11763, #15541, #36002, #969 ) ) ;
#43207=CARTESIAN_POINT ( 'NONE',  ( 85.82015659721905365, -25.23119213852205789, -15.24166438581092109 ) ) ;
#43211=CARTESIAN_POINT ( 'NONE',  ( 94.20708369096698220, -25.99489077589524300, -13.39321520033831447 ) ) ;
#43219=DIRECTION ( 'NONE',  ( 0.000000000000000000, 0.3818493186865927203, -0.9242245927363029745 ) ) ;
#43220=EDGE_CURVE ( 'NONE', #1042, #43595, #9231, .T. ) ;
#43238=DIRECTION ( 'NONE',  ( -1.000000000000000000, 0.000000000000000000, 0.000000000000000000 ) ) ;
#43247=ADVANCED_FACE ( 'NONE', ( #3268 ), #13985, .T. ) ;
#43249=DIRECTION ( 'NONE',  ( 1.000000000000000000, 0.000000000000000000, -0.000000000000000000 ) ) ;
#43251=CARTESIAN_POINT ( 'NONE',  ( 91.11246428952674137, -26.75858941326842810, -11.54476601486570964 ) ) ;
#43274=FACE_OUTER_BOUND ( 'NONE', #11354, .T. ) ;
#43286=CARTESIAN_POINT ( 'NONE',  ( 83.83554121260367253, -25.99489077589524300, -13.39321520033831625 ) ) ;
#43289=ADVANCED_FACE ( 'NONE', ( #18073 ), #3403, .T. ) ;
#43322=DIRECTION ( 'NONE',  ( -1.224775218828351862E-16, 0.9242245927363029745, 0.3818493186865928868 ) ) ;
#43333=DIRECTION ( 'NONE',  ( 1.000000000000000000, 0.000000000000000000, -0.000000000000000000 ) ) ;
#43345=DIRECTION ( 'NONE',  ( 0.000000000000000000, 0.3818493186865927203, -0.9242245927363029745 ) ) ;
#43378=EDGE_LOOP ( 'NONE', ( #209, #33373, #41541, #29916, #618 ) ) ;
#43381=CONICAL_SURFACE ( 'NONE', #9908, 1.610000000000000986, 0.9599310885968765916 ) ;
#43388=ORIENTED_EDGE ( 'NONE', *, *, #10263, .F. ) ;
#43389=AXIS2_PLACEMENT_3D ( 'NONE', #27688, #45019, #6485 ) ;
#43399=LINE ( 'NONE', #16948, #43083 ) ;
#43420=VECTOR ( 'NONE', #45133, 1000.000000000000000 ) ;
#43447=FACE_OUTER_BOUND ( 'NONE', #27117, .T. ) ;
#43465=CARTESIAN_POINT ( 'NONE',  ( 85.82015659721905365, -25.99489077589524300, -13.39321520033831625 ) ) ;
#43481=AXIS2_PLACEMENT_3D ( 'NONE', #6714, #9916, #20624 ) ;
#43490=ADVANCED_FACE ( 'NONE', ( #5053 ), #11911, .T. ) ;
#43491=DIRECTION ( 'NONE',  ( 0.000000000000000000, -0.9242245927363027524, -0.3818493186865928868 ) ) ;
#43499=CARTESIAN_POINT ( 'NONE',  ( 84.38170309240724976, -25.99489077589524300, -13.39321520033831447 ) ) ;
#43539=ORIENTED_EDGE ( 'NONE', *, *, #11060, .F. ) ;
#43544=ORIENTED_EDGE ( 'NONE', *, *, #10288, .T. ) ;
#43595=VERTEX_POINT ( 'NONE', #25592 ) ;
#43611=ORIENTED_EDGE ( 'NONE', *, *, #1593, .F. ) ;
#43690=EDGE_CURVE ( 'NONE', #4544, #2844, #6866, .T. ) ;
#43693=ORIENTED_EDGE ( 'NONE', *, *, #35105, .T. ) ;
#43703=B_SPLINE_CURVE_WITH_KNOTS ( 'NONE', 3,
 ( #26841, #43946, #40527, #33653 ),
 .UNSPECIFIED., .F., .F.,
 ( 4, 4 ),
 ( 0.000000000000000000, 1.000000000000000000 ),
 .UNSPECIFIED. ) ;
#43705=AXIS2_PLACEMENT_3D ( 'NONE', #8356, #26131, #36603 ) ;
#43709=DIRECTION ( 'NONE',  ( 0.5735764363510498232, -0.3127926500124802445, 0.7570804645221007600 ) ) ;
#43743=DIRECTION ( 'NONE',  ( 1.000000000000000000, 0.000000000000000000, -0.000000000000000000 ) ) ;
#43745=ORIENTED_EDGE ( 'NONE', *, *, #42664, .T. ) ;
#43753=VERTEX_POINT ( 'NONE', #32746 ) ;
#43756=ORIENTED_EDGE ( 'NONE', *, *, #38937, .F. ) ;
#43764=AXIS2_PLACEMENT_3D ( 'NONE', #40316, #32337, #15021 ) ;
#43770=CARTESIAN_POINT ( 'NONE',  ( 94.20708369096698220, -25.99489077589524300, -13.39321520033831447 ) ) ;
#43775=CARTESIAN_POINT ( 'NONE',  ( 85.70478001548416103, -25.23119213852205789, -15.24166438581092109 ) ) ;
#43781=CARTESIAN_POINT ( 'NONE',  ( 86.36631847702263087, -25.99489077589524300, -13.39321520033831447 ) ) ;
#43802=CARTESIAN_POINT ( 'NONE',  ( 85.04324155394569118, -25.23119213852205789, -15.24166438581092109 ) ) ;
#43808=ORIENTED_EDGE ( 'NONE', *, *, #30047, .T. ) ;
#43810=AXIS2_PLACEMENT_3D ( 'NONE', #1164, #18945, #43345 ) ;
#43820=( GEOMETRIC_REPRESENTATION_CONTEXT ( 3 ) GLOBAL_UNCERTAINTY_ASSIGNED_CONTEXT ( ( #14645 ) ) GLOBAL_UNIT_ASSIGNED_CONTEXT ( ( #31677, #40907, #44549 ) ) REPRESENTATION_CONTEXT ( 'NONE', 'WORKASPACE' ) );
#43831=CONICAL_SURFACE ( 'NONE', #25637, 3077.683537175320453, 1.256637061435923686 ) ;
#43835=ORIENTED_EDGE ( 'NONE', *, *, #35841, .T. ) ;
#43838=AXIS2_PLACEMENT_3D ( 'NONE', #42161, #39176, #42609 ) ;
#43862=DIRECTION ( 'NONE',  ( 1.000000000000000000, 0.000000000000000000, -0.000000000000000000 ) ) ;
#43880=CARTESIAN_POINT ( 'NONE',  ( 91.38554522942851577, -25.99489077589524300, -13.39321520033831625 ) ) ;
#43887=AXIS2_PLACEMENT_3D ( 'NONE', #4541, #32129, #1344 ) ;
#43914=DIRECTION ( 'NONE',  ( 1.000000000000000000, 0.000000000000000000, -0.000000000000000000 ) ) ;
#43928=AXIS2_PLACEMENT_3D ( 'NONE', #9693, #13347, #35574 ) ;
#43946=CARTESIAN_POINT ( 'NONE',  ( 95.62170725701130891, -25.45311294428598003, -12.61215234878372726 ) ) ;
#43948=EDGE_CURVE ( 'NONE', #22604, #27606, #42044, .T. ) ;
#43950=AXIS2_PLACEMENT_3D ( 'NONE', #5153, #29557, #39821 ) ;
#43980=ADVANCED_FACE ( 'NONE', ( #13157 ), #25275, .F. ) ;
#44020=VERTEX_POINT ( 'NONE', #1022 ) ;
#44030=DIRECTION ( 'NONE',  ( 1.000000000000000000, 0.000000000000000000, -0.000000000000000000 ) ) ;
#44051=ORIENTED_EDGE ( 'NONE', *, *, #8673, .F. ) ;
#44057=ORIENTED_EDGE ( 'NONE', *, *, #36154, .T. ) ;
#44063=CARTESIAN_POINT ( 'NONE',  ( 121.9470836909669913, -25.99489077589524300, -13.39321520033831447 ) ) ;
#44090=AXIS2_PLACEMENT_3D ( 'NONE', #7132, #6703, #3927 ) ;
#44092=CARTESIAN_POINT ( 'NONE',  ( 93.44708369096697709, -28.02818487991510921, -14.23328370144882093 ) ) ;
#44117=CIRCLE ( 'NONE', #39738, 0.8509999999999994236 ) ;
#44128=ORIENTED_EDGE ( 'NONE', *, *, #37835, .F. ) ;
#44140=CARTESIAN_POINT ( 'NONE',  ( 89.67401078471493747, -25.99489077589524300, -13.39321520033831447 ) ) ;
#44144=CARTESIAN_POINT ( 'NONE',  ( 87.14323352029596492, -25.23119213852205789, -15.24166438581092109 ) ) ;
#44147=CARTESIAN_POINT ( 'NONE',  ( 90.06246830635160450, -26.60966817898065884, -11.90521360603286816 ) ) ;
#44180=EDGE_CURVE ( 'NONE', #9192, #44761, #10470, .T. ) ;
#44206=ORIENTED_EDGE ( 'NONE', *, *, #36723, .T. ) ;
#44215=EDGE_LOOP ( 'NONE', ( #15152, #13243, #3711, #38359, #26172, #10021, #26646, #22740, #4156, #32191, #18644, #13936, #28733 ) ) ;
#44229=DIRECTION ( 'NONE',  ( 1.000000000000000000, 0.000000000000000000, -0.000000000000000000 ) ) ;
#44274=EDGE_CURVE ( 'NONE', #9931, #21884, #2711, .T. ) ;
#44289=VERTEX_POINT ( 'NONE', #32538 ) ;
#44313=ORIENTED_EDGE ( 'NONE', *, *, #12029, .T. ) ;
#44321=DIRECTION ( 'NONE',  ( 0.000000000000000000, -0.3818493186865927203, 0.9242245927363029745 ) ) ;
#44323=ORIENTED_EDGE ( 'NONE', *, *, #11060, .T. ) ;
#44325=CARTESIAN_POINT ( 'NONE',  ( 84.10862215250544693, -25.99489077589524300, -13.39321520033831625 ) ) ;
#44345=ORIENTED_EDGE ( 'NONE', *, *, #790, .F. ) ;
#44352=ORIENTED_EDGE ( 'NONE', *, *, #38003, .F. ) ;
#44371=DIRECTION ( 'NONE',  ( -0.5735764363510446051, 0.3127926500124816878, -0.7570804645221042017 ) ) ;
#44378=LINE ( 'NONE', #6050, #40855 ) ;
#44395=EDGE_LOOP ( 'NONE', ( #34710, #16694 ) ) ;
#44414=LINE ( 'NONE', #20913, #22635 ) ;
#44419=CARTESIAN_POINT ( 'NONE',  ( 96.46827370896536991, -25.99489077589524300, -13.39321520033831447 ) ) ;
#44422=VECTOR ( 'NONE', #1815, 1000.000000000000114 ) ;
#44438=ADVANCED_FACE ( 'NONE', ( #29578 ), #26028, .T. ) ;
#44446=FACE_OUTER_BOUND ( 'NONE', #36459, .T. ) ;
#44453=CIRCLE ( 'NONE', #24779, 2.000000000000000444 ) ;
#44472=CARTESIAN_POINT ( 'NONE',  ( 85.04324155394569118, -24.14644159042263993, -12.62951656296512937 ) ) ;
#44473=LINE ( 'NONE', #16432, #8705 ) ;
#44480=CARTESIAN_POINT ( 'NONE',  ( 88.46631044337289040, -25.99489077589524300, -13.39321520033831625 ) ) ;
#44488=AXIS2_PLACEMENT_3D ( 'NONE', #19845, #2504, #26910 ) ;
#44511=CYLINDRICAL_SURFACE ( 'NONE', #14129, 1.999999999999998890 ) ;
#44542=VERTEX_POINT ( 'NONE', #38823 ) ;
#44549=( NAMED_UNIT ( * ) SI_UNIT ( $, .STERADIAN. ) SOLID_ANGLE_UNIT ( ) );
#44573=CARTESIAN_POINT ( 'NONE',  ( 89.78938736644981589, -25.23119213852205789, -15.24166438581092109 ) ) ;
#44580=ORIENTED_EDGE ( 'NONE', *, *, #41842, .F. ) ;
#44614=PRODUCT_CONTEXT ( 'NONE', #30024, 'mechanical' ) ;
#44619=CIRCLE ( 'NONE', #8931, 2.000000000000000444 ) ;
#44636=DIRECTION ( 'NONE',  ( 1.000000000000000000, 0.000000000000000000, -0.000000000000000000 ) ) ;
#44649=CARTESIAN_POINT ( 'NONE',  ( 95.28169473643895060, -25.99489077589524300, -13.39321520033831447 ) ) ;
#44652=CIRCLE ( 'NONE', #20601, 2.000000000000000444 ) ;
#44656=ORIENTED_EDGE ( 'NONE', *, *, #4213, .F. ) ;
#44663=CARTESIAN_POINT ( 'NONE',  ( 93.24708369096698846, -23.96159667187537679, -12.55314669922780979 ) ) ;
#44709=CARTESIAN_POINT ( 'NONE',  ( 121.9470836909669913, -25.99489077589524300, -13.39321520033831447 ) ) ;
#44721=ADVANCED_FACE ( 'NONE', ( #7970 ), #33186, .T. ) ;
#44738=EDGE_LOOP ( 'NONE', ( #17823, #11860, #13439, #17540, #3935, #28457 ) ) ;
#44753=EDGE_LOOP ( 'NONE', ( #11740, #20399, #32048, #16031, #19645 ) ) ;
#44761=VERTEX_POINT ( 'NONE', #21207 ) ;
#44786=DIRECTION ( 'NONE',  ( 0.000000000000000000, 0.9242245927363040847, 0.3818493186865896671 ) ) ;
#44807=EDGE_CURVE ( 'NONE', #7405, #20846, #1178, .T. ) ;
#44811=DIRECTION ( 'NONE',  ( 0.000000000000000000, -0.9242245927363029745, -0.3818493186865927203 ) ) ;
#44819=EDGE_CURVE ( 'NONE', #43595, #9931, #24631, .T. ) ;
#44836=EDGE_CURVE ( 'NONE', #26941, #39210, #11178, .T. ) ;
#44846=EDGE_CURVE ( 'NONE', #8410, #44542, #8198, .T. ) ;
#44860=CARTESIAN_POINT ( 'NONE',  ( 94.86797725101182266, -26.75172757040932936, -12.91007389524920157 ) ) ;
#44866=ORIENTED_EDGE ( 'NONE', *, *, #14431, .F. ) ;
#44869=DIRECTION ( 'NONE',  ( -1.000000000000000000, 0.000000000000000000, 0.000000000000000000 ) ) ;
#44871=CIRCLE ( 'NONE', #39022, 1.610000000000000986 ) ;
#44889=EDGE_LOOP ( 'NONE', ( #9792, #33532, #16921, #41120, #25755, #34660 ) ) ;
#44893=CIRCLE ( 'NONE', #19377, 2.000000000000000444 ) ;
#44904=CONICAL_SURFACE ( 'NONE', #28875, 2.000000000000000444, 0.9599310885968830309 ) ;
#44907=VERTEX_POINT ( 'NONE', #35085 ) ;
#44924=ORIENTED_EDGE ( 'NONE', *, *, #16387, .F. ) ;
#44927=AXIS2_PLACEMENT_3D ( 'NONE', #23854, #6511, #20426 ) ;
#44928=LINE ( 'NONE', #13686, #11019 ) ;
#44932=ORIENTED_EDGE ( 'NONE', *, *, #44836, .T. ) ;
#44942=FACE_OUTER_BOUND ( 'NONE', #43196, .T. ) ;
#44951=DIRECTION ( 'NONE',  ( 0.5735764363510499342, 0.3127926500124801890, -0.7570804645221008711 ) ) ;
#44985=ORIENTED_EDGE ( 'NONE', *, *, #35361, .F. ) ;
#45008=FACE_OUTER_BOUND ( 'NONE', #480, .T. ) ;
#45012=ORIENTED_EDGE ( 'NONE', *, *, #39499, .T. ) ;
#45019=DIRECTION ( 'NONE',  ( -0.4461977533474358326, -0.3417300876246960328, 0.8271203734159366938 ) ) ;
#45026=ORIENTED_EDGE ( 'NONE', *, *, #27126, .F. ) ;
#45035=DIRECTION ( 'NONE',  ( 1.000000000000000000, 0.000000000000000000, -0.000000000000000000 ) ) ;
#45076=CARTESIAN_POINT ( 'NONE',  ( 94.20708369096698220, -25.28273535805287864, -12.54175975618893091 ) ) ;
#45086=EDGE_CURVE ( 'NONE', #24250, #9155, #36668, .T. ) ;
#45095=CARTESIAN_POINT ( 'NONE',  ( 88.46631044337289040, -25.99489077589524300, -13.39321520033831625 ) ) ;
#45097=LINE ( 'NONE', #33910, #24792 ) ;
#45115=CARTESIAN_POINT ( 'NONE',  ( 91.11246428952674137, -27.84333996136784961, -14.15691383771150136 ) ) ;
#45120=EDGE_CURVE ( 'NONE', #2844, #35171, #27393, .T. ) ;
#45125=LINE ( 'NONE', #17314, #481 ) ;
#45133=DIRECTION ( 'NONE',  ( 1.000000000000000000, 0.000000000000000000, -0.000000000000000000 ) ) ;
#45141=ORIENTED_EDGE ( 'NONE', *, *, #21941, .F. ) ;
#45146=AXIS2_PLACEMENT_3D ( 'NONE', #1804, #2257, #40810 ) ;
#45184=COLOUR_RGB('Black',0.12,0.14,0.17);
#45185=FILL_AREA_STYLE_COLOUR('',#45184);
#45186=FILL_AREA_STYLE('',(#45185));
#45187=SURFACE_STYLE_FILL_AREA(#45186);
#45188=SURFACE_SIDE_STYLE('',(#45187));
#45189=SURFACE_STYLE_USAGE(.BOTH.,#45188);
#45190=PRESENTATION_STYLE_ASSIGNMENT((#45189));
ENDSEC;
END-ISO-10303-21;
